ISO-10303-21;
HEADER;
FILE_DESCRIPTION (('STEP AP214'),
    '1' );
FILE_NAME ('torque nut 04-2_iso_ISO 7043-M5-N.step',
    '2026-09-24T10:28:59',
    ( '' ),
    ( '' ),
    'SwSTEP 2.0',
    'SolidWorks 2026',
    '' );
FILE_SCHEMA (( 'AUTOMOTIVE_DESIGN' ));
ENDSEC;

DATA;
#11=CARTESIAN_POINT ( 'NONE',  ( 0.5636734750061580534, 4.293365120987025385, -3.231543764079864101 ) ) ;
#12=CARTESIAN_POINT ( 'NONE',  ( -4.140405595019059248, -2.228337868678524458, -3.386887224136967411 ) ) ;
#27=EDGE_CURVE ( 'NONE', #7462, #10575, #2062, .T. ) ;
#53=CARTESIAN_POINT ( 'NONE',  ( -7.511572993685817836E-16, -4.618802153517020059, -3.133295621305386636 ) ) ;
#54=PRESENTATION_STYLE_ASSIGNMENT (( #17863 ) ) ;
#86=CARTESIAN_POINT ( 'NONE',  ( 0.000000000000000000, 0.000000000000000000, -4.700000000000000178 ) ) ;
#96=CARTESIAN_POINT ( 'NONE',  ( -4.000000000000000000, 2.309401076758501592, -0.4999999999999963363 ) ) ;
#100=AXIS2_PLACEMENT_3D ( 'NONE', #12940, #16861, #525 ) ;
#131=VERTEX_POINT ( 'NONE', #5429 ) ;
#187=( BOUNDED_SURFACE ( )  B_SPLINE_SURFACE ( 3, 2, ( 
 ( #15565, #5853, #6132 ),
 ( #7149, #10017, #8682 ),
 ( #15660, #7420, #17130 ),
 ( #8776, #4680, #7501 ),
 ( #518, #1619, #4589 ),
 ( #14209, #7333, #249 ) ),
 .UNSPECIFIED., .F., .F., .T. ) 
 B_SPLINE_SURFACE_WITH_KNOTS ( ( 4, 2, 4 ),
 ( 3, 3 ),
 ( 0.02018906359535397113, 0.02264947622839649788, 0.02510988886143902810 ),
 ( 0.000000000000000000, 1.000000000000000000 ),
 .UNSPECIFIED. ) 
 GEOMETRIC_REPRESENTATION_ITEM ( )  RATIONAL_B_SPLINE_SURFACE ( (
 ( 1.000000000000000000, 0.8047781357041529082, 1.000000000000000000),
 ( 1.000000000000000000, 0.8123775905861528868, 1.000000000000000000),
 ( 1.000000000000000000, 0.8190671519372876297, 1.000000000000000000),
 ( 1.000000000000000000, 0.8192352278312100555, 1.000000000000000000),
 ( 1.000000000000000000, 0.8126131206996280998, 1.000000000000000000),
 ( 1.000000000000000000, 0.8047712494894333490, 1.000000000000000000) ) ) 
 REPRESENTATION_ITEM ( '' )  SURFACE ( )  );
#197=DIRECTION ( 'NONE',  ( -1.000000000000000000, 0.000000000000000000, 0.000000000000000000 ) ) ;
#223=ORIENTED_EDGE ( 'NONE', *, *, #9237, .T. ) ;
#234=DIRECTION ( 'NONE',  ( 1.000000000000000000, 0.000000000000000000, 0.000000000000000000 ) ) ;
#241=ORIENTED_EDGE ( 'NONE', *, *, #27, .F. ) ;
#243=DIRECTION ( 'NONE',  ( 0.000000000000000000, 0.000000000000000000, -1.000000000000000000 ) ) ;
#249=CARTESIAN_POINT ( 'NONE',  ( -4.211405941597130109, -2.460460478483078361, -3.451298436431160077 ) ) ;
#258=CARTESIAN_POINT ( 'NONE',  ( 0.000000000000000000, 0.000000000000000000, -4.394516984716110741 ) ) ;
#271=PLANE ( 'NONE',  #2587 ) ;
#283=LINE ( 'NONE', #14248, #9848 ) ;
#300=ORIENTED_EDGE ( 'NONE', *, *, #10123, .T. ) ;
#302=CARTESIAN_POINT ( 'NONE',  ( -0.6507732100473456738, 4.243078065514776398, -0.2236248678334832318 ) ) ;
#308=ORIENTED_EDGE ( 'NONE', *, *, #12713, .F. ) ;
#339=ORIENTED_EDGE ( 'NONE', *, *, #15948, .F. ) ;
#364=VERTEX_POINT ( 'NONE', #16969 ) ;
#418=CARTESIAN_POINT ( 'NONE',  ( 0.000000000000000000, 0.000000000000000000, 13.31572692736085095 ) ) ;
#442=DIRECTION ( 'NONE',  ( 1.000000000000000000, 0.000000000000000000, 0.000000000000000000 ) ) ;
#463=LINE ( 'NONE', #8609, #11325 ) ;
#464=FACE_OUTER_BOUND ( 'NONE', #9098, .T. ) ;
#469=CARTESIAN_POINT ( 'NONE',  ( 4.207491450040567571, -2.029819825146481183, -3.371670828759568028 ) ) ;
#483=CARTESIAN_POINT ( 'NONE',  ( 3.035766082959412415E-15, 4.618802153517010289, -0.5000000000000000000 ) ) ;
#508=AXIS2_PLACEMENT_3D ( 'NONE', #1126, #17848, #9453 ) ;
#514=DIRECTION ( 'NONE',  ( 0.000000000000000000, 0.000000000000000000, -1.000000000000000000 ) ) ;
#516=ORIENTED_EDGE ( 'NONE', *, *, #8838, .F. ) ;
#517=CARTESIAN_POINT ( 'NONE',  ( 4.000000000000000000, -1.560351142792949064, -0.2242961665059824972 ) ) ;
#518=CARTESIAN_POINT ( 'NONE',  ( -4.000000000000000000, -1.680125368658796692, -3.016613018637368970 ) ) ;
#525=DIRECTION ( 'NONE',  ( -1.000000000000000000, 1.224646799147352714E-16, 0.000000000000000000 ) ) ;
#540=PLANE ( 'NONE',  #12777 ) ;
#552=CARTESIAN_POINT ( 'NONE',  ( -4.000000000000000000, -2.309401076758508253, -4.700000000000000178 ) ) ;
#553=CARTESIAN_POINT ( 'NONE',  ( 4.204015924366189871, -1.626724848190929551, -3.310627190413393262 ) ) ;
#581=CARTESIAN_POINT ( 'NONE',  ( -1.654252653721908661, -3.663718938583020446, -0.01223254789874225583 ) ) ;
#584=ORIENTED_EDGE ( 'NONE', *, *, #1543, .T. ) ;
#603=EDGE_CURVE ( 'NONE', #11660, #14159, #14693, .T. ) ;
#611=CARTESIAN_POINT ( 'NONE',  ( 4.000000000000000000, -1.942223658245632256, -0.3516579909967657569 ) ) ;
#633=AXIS2_PLACEMENT_3D ( 'NONE', #8229, #4240, #15388 ) ;
#635=CIRCLE ( 'NONE', #9875, 3.999999999999998224 ) ;
#648=AXIS2_PLACEMENT_3D ( 'NONE', #5014, #7832, #13096 ) ;
#658=CARTESIAN_POINT ( 'NONE',  ( 4.236525418537981480, -2.416953631397932956, -3.451298686683626826 ) ) ;
#683=LINE ( 'NONE', #769, #6632 ) ;
#694=ORIENTED_EDGE ( 'NONE', *, *, #968, .F. ) ;
#697=CARTESIAN_POINT ( 'NONE',  ( -2.000000000000005329, -3.464101615137750390, 0.000000000000000000 ) ) ;
#719=CARTESIAN_POINT ( 'NONE',  ( 0.000000000000000000, 0.000000000000000000, -4.700000000000000178 ) ) ;
#732=ORIENTED_EDGE ( 'NONE', *, *, #3449, .F. ) ;
#734=ADVANCED_FACE ( 'NONE', ( #15433 ), #10728, .F. ) ;
#758=CARTESIAN_POINT ( 'NONE',  ( -4.211140560182196957, 2.431303136016540911, -3.445885042887435468 ) ) ;
#759=CARTESIAN_POINT ( 'NONE',  ( 2.682243648011665371, 3.070208061305305769, -0.04852650426601385486 ) ) ;
#768=CARTESIAN_POINT ( 'NONE',  ( -4.211140560182196957, -2.431303136016548017, -3.445885042887436356 ) ) ;
#769=CARTESIAN_POINT ( 'NONE',  ( 4.000000000000000000, 0.000000000000000000, 13.31572692736085095 ) ) ;
#776=ORIENTED_EDGE ( 'NONE', *, *, #8484, .T. ) ;
#783=CARTESIAN_POINT ( 'NONE',  ( 3.999999999999998224, -2.309401076758513582, -0.5000000000000000000 ) ) ;
#787=CARTESIAN_POINT ( 'NONE',  ( -3.333333333333334370, 2.694301256218252671, -3.000726591567082213 ) ) ;
#794=CIRCLE ( 'NONE', #17025, 2.500000000000000888 ) ;
#795=ADVANCED_FACE ( 'NONE', ( #4080 ), #8157, .T. ) ;
#802=AXIS2_PLACEMENT_3D ( 'NONE', #6740, #12276, #16535 ) ;
#816=CARTESIAN_POINT ( 'NONE',  ( 1.999999999999997113, -3.464101615137767265, -2.842992957459238301 ) ) ;
#830=DIRECTION ( 'NONE',  ( 0.000000000000000000, 0.000000000000000000, 1.000000000000000000 ) ) ;
#831=CIRCLE ( 'NONE', #13854, 2.100000000000000089 ) ;
#833=UNCERTAINTY_MEASURE_WITH_UNIT (LENGTH_MEASURE( 1.000000000000000082E-05 ), #16057, 'distance_accuracy_value', 'NONE');
#834=B_SPLINE_CURVE_WITH_KNOTS ( 'NONE', 3,
 ( #13075, #6361, #11976, #3651, #9089 ),
 .UNSPECIFIED., .F., .F.,
 ( 4, 1, 4 ),
 ( 0.000000000000000000, 0.002309401076758504923, 0.004618802153517009845 ),
 .UNSPECIFIED. ) ;
#839=CARTESIAN_POINT ( 'NONE',  ( 1.274241539467174222, 3.883118457693031544, -2.920601398289339290 ) ) ;
#853=AXIS2_PLACEMENT_3D ( 'NONE', #5515, #12329, #5425 ) ;
#872=EDGE_LOOP ( 'NONE', ( #16482, #13796, #4156, #9248 ) ) ;
#889=ADVANCED_FACE ( 'NONE', ( #8168 ), #13700, .F. ) ;
#893=EDGE_LOOP ( 'NONE', ( #5361, #16625 ) ) ;
#914=CIRCLE ( 'NONE', #1211, 3.000000000000000000 ) ;
#926=CARTESIAN_POINT ( 'NONE',  ( 1.243833333692658361, -3.900674643482532122, -2.923144239647436304 ) ) ;
#935=ADVANCED_FACE ( 'NONE', ( #16509 ), #13868, .T. ) ;
#944=EDGE_LOOP ( 'NONE', ( #3210, #11265, #10421, #10951, #13756 ) ) ;
#950=AXIS2_PLACEMENT_3D ( 'NONE', #9550, #2681, #10089 ) ;
#968=EDGE_CURVE ( 'NONE', #2889, #16703, #5054, .T. ) ;
#971=DIRECTION ( 'NONE',  ( -0.000000000000000000, -0.000000000000000000, 1.000000000000000000 ) ) ;
#994=( BOUNDED_SURFACE ( )  B_SPLINE_SURFACE ( 3, 2, ( 
 ( #12064, #10687, #6368 ),
 ( #2217, #16265, #14548 ),
 ( #2130, #14636, #10528 ),
 ( #839, #14889, #11891 ),
 ( #17471, #11, #5346 ),
 ( #9433, #4273, #2817 ) ),
 .UNSPECIFIED., .F., .F., .T. ) 
 B_SPLINE_SURFACE_WITH_KNOTS ( ( 4, 2, 4 ),
 ( 3, 3 ),
 ( 0.02023740217035200836, 0.02269762987400599299, 0.02515785757765997763 ),
 ( 0.000000000000000000, 1.000000000000000000 ),
 .UNSPECIFIED. ) 
 GEOMETRIC_REPRESENTATION_ITEM ( )  RATIONAL_B_SPLINE_SURFACE ( (
 ( 1.000000000000000000, 0.8047781539129733597, 1.000000000000000000),
 ( 1.000000000000000000, 0.8123770319056771161, 1.000000000000000000),
 ( 1.000000000000000000, 0.8190663783057344771, 1.000000000000000000),
 ( 1.000000000000000000, 0.8192359702876569338, 1.000000000000000000),
 ( 1.000000000000000000, 0.8126134888420186719, 1.000000000000000000),
 ( 1.000000000000000000, 0.8047712368238110203, 1.000000000000000000) ) ) 
 REPRESENTATION_ITEM ( '' )  SURFACE ( )  );
#1018=CARTESIAN_POINT ( 'NONE',  ( 3.436326524993535081, -2.634838109287350516, -3.231543764078689929 ) ) ;
#1033=B_SPLINE_CURVE_WITH_KNOTS ( 'NONE', 3,
 ( #3064, #12661, #14211, #17229, #11661, #4768, #11469, #7150 ),
 .UNSPECIFIED., .F., .F.,
 ( 4, 2, 2, 4 ),
 ( 1.451928974504550231E-19, 0.002450665683189817961, 0.003675998524784728459, 0.004901331366379638524 ),
 .UNSPECIFIED. ) ;
#1037=CARTESIAN_POINT ( 'NONE',  ( -2.540000000000001368, 3.110602869834278640E-16, 1.599999999999998979 ) ) ;
#1062=DIRECTION ( 'NONE',  ( -0.000000000000000000, -0.000000000000000000, 1.000000000000000000 ) ) ;
#1065=CARTESIAN_POINT ( 'NONE',  ( 0.000000000000000000, 0.000000000000000000, 0.000000000000000000 ) ) ;
#1084=EDGE_CURVE ( 'NONE', #9477, #14231, #5339, .T. ) ;
#1103=CARTESIAN_POINT ( 'NONE',  ( 2.000000000000002220, 3.464101615137753054, -2.842992957459234304 ) ) ;
#1106=CARTESIAN_POINT ( 'NONE',  ( 1.828356344711638881, 3.563200125723181344, -1.227350740571481191E-15 ) ) ;
#1108=CARTESIAN_POINT ( 'NONE',  ( -0.5449245075114568237, -4.304189842417255996, -3.016622336522495118 ) ) ;
#1124=CARTESIAN_POINT ( 'NONE',  ( 0.000000000000000000, 0.000000000000000000, -4.674599999999997202 ) ) ;
#1126=CARTESIAN_POINT ( 'NONE',  ( 0.000000000000000000, 0.000000000000000000, -4.674599999999997202 ) ) ;
#1144=CARTESIAN_POINT ( 'NONE',  ( -4.175647895129166898, 2.207990717223085930, -3.169390900447850878 ) ) ;
#1171=EDGE_LOOP ( 'NONE', ( #9781, #9162 ) ) ;
#1211=AXIS2_PLACEMENT_3D ( 'NONE', #12487, #8755, #7400 ) ;
#1213=DIRECTION ( 'NONE',  ( 1.000000000000000000, 0.000000000000000000, 0.000000000000000000 ) ) ;
#1214=ORIENTED_EDGE ( 'NONE', *, *, #5761, .F. ) ;
#1224=CYLINDRICAL_SURFACE ( 'NONE', #802, 2.500000000000000888 ) ;
#1243=DIRECTION ( 'NONE',  ( 0.000000000000000000, 0.000000000000000000, -1.000000000000000000 ) ) ;
#1283=CARTESIAN_POINT ( 'NONE',  ( 0.000000000000000000, 0.000000000000000000, 13.31572692736085095 ) ) ;
#1314=CARTESIAN_POINT ( 'NONE',  ( -4.204015924366189871, 1.626724848190924444, -3.310627190413392817 ) ) ;
#1321=EDGE_CURVE ( 'NONE', #14985, #12543, #4242, .T. ) ;
#1374=CARTESIAN_POINT ( 'NONE',  ( 0.02511946470933708320, -4.877415451931371493, -3.451298686683631267 ) ) ;
#1378=EDGE_CURVE ( 'NONE', #7023, #9939, #914, .T. ) ;
#1380=ORIENTED_EDGE ( 'NONE', *, *, #3345, .T. ) ;
#1382=CARTESIAN_POINT ( 'NONE',  ( 4.000000000000000000, 2.309401076758498483, -3.133295621305380863 ) ) ;
#1393=AXIS2_PLACEMENT_3D ( 'NONE', #2284, #2110, #15698 ) ;
#1396=( GEOMETRIC_REPRESENTATION_CONTEXT ( 3 ) GLOBAL_UNCERTAINTY_ASSIGNED_CONTEXT ( ( #833 ) ) GLOBAL_UNIT_ASSIGNED_CONTEXT ( ( #16057, #16484, #3972 ) ) REPRESENTATION_CONTEXT ( 'NONE', 'WORKASPACE' ) );
#1397=CIRCLE ( 'NONE', #8065, 0.8000000000000001554 ) ;
#1409=DIRECTION ( 'NONE',  ( -0.000000000000000000, -0.000000000000000000, 1.000000000000000000 ) ) ;
#1429=CARTESIAN_POINT ( 'NONE',  ( -4.000000000000000000, 2.309401076758501592, -4.700000000000000178 ) ) ;
#1435=CARTESIAN_POINT ( 'NONE',  ( 3.999999999999998224, -2.309401076758513582, -0.5000000000000000000 ) ) ;
#1479=ORIENTED_EDGE ( 'NONE', *, *, #15032, .T. ) ;
#1480=SHAPE_REPRESENTATION ( 'torque nut 04-2_iso_ISO 7043-M5-N', ( #3575 ), #4782 ) ;
#1486=CARTESIAN_POINT ( 'NONE',  ( 4.000000000000000000, -1.677829075513255219, -3.235264651232380828 ) ) ;
#1509=DIRECTION ( 'NONE',  ( -1.000000000000000000, 0.000000000000000000, 0.000000000000000000 ) ) ;
#1510=B_SPLINE_CURVE_WITH_KNOTS ( 'NONE', 3,
 ( #5461, #2674, #14995, #1314, #8204, #13731 ),
 .UNSPECIFIED., .F., .F.,
 ( 4, 2, 4 ),
 ( 0.002452478801916373706, 0.003676905084148006115, 0.004901331366379638524 ),
 .UNSPECIFIED. ) ;
#1518=EDGE_CURVE ( 'NONE', #16729, #10872, #9361, .T. ) ;
#1537=ORIENTED_EDGE ( 'NONE', *, *, #3910, .T. ) ;
#1543=EDGE_CURVE ( 'NONE', #4061, #16703, #10741, .T. ) ;
#1619=CARTESIAN_POINT ( 'NONE',  ( -4.000000000000000888, -1.658477411508030519, -3.231534348142504509 ) ) ;
#1623=PLANE ( 'NONE',  #3574 ) ;
#1634=ORIENTED_EDGE ( 'NONE', *, *, #10733, .T. ) ;
#1642=CARTESIAN_POINT ( 'NONE',  ( -2.171643655288370667, 3.365003104552323876, -2.116735335188496547E-15 ) ) ;
#1644=CARTESIAN_POINT ( 'NONE',  ( -2.038300084272748336E-14, -4.618802153517010289, -0.5000000000000000000 ) ) ;
#1645=CARTESIAN_POINT ( 'NONE',  ( -5.560781378645575757, 6.809993116116508640E-16, -3.700000000000000178 ) ) ;
#1657=ORIENTED_EDGE ( 'NONE', *, *, #13824, .T. ) ;
#1665=DIRECTION ( 'NONE',  ( 1.000000000000000000, 0.000000000000000000, -0.000000000000000000 ) ) ;
#1689=EDGE_CURVE ( 'NONE', #4375, #14985, #834, .T. ) ;
#1694=ORIENTED_EDGE ( 'NONE', *, *, #10152, .T. ) ;
#1698=DIRECTION ( 'NONE',  ( -1.000000000000000000, 0.000000000000000000, 0.000000000000000000 ) ) ;
#1721=ORIENTED_EDGE ( 'NONE', *, *, #9838, .F. ) ;
#1723=CONICAL_SURFACE ( 'NONE', #8085, 5.560781378645573980, 1.221730476396047926 ) ;
#1746=AXIS2_PLACEMENT_3D ( 'NONE', #7236, #16945, #11562 ) ;
#1748=ADVANCED_FACE ( 'NONE', ( #3831 ), #7240, .F. ) ;
#1807=CARTESIAN_POINT ( 'NONE',  ( 4.000000000000000000, -2.309401076758510918, -3.133295621305383083 ) ) ;
#1886=CARTESIAN_POINT ( 'NONE',  ( -2.100000000000000089, 2.571758278209441957E-16, 1.159999999999999476 ) ) ;
#1922=DIRECTION ( 'NONE',  ( 1.000000000000000000, 0.000000000000000000, 0.000000000000000000 ) ) ;
#1926=CARTESIAN_POINT ( 'NONE',  ( 0.000000000000000000, 0.000000000000000000, 1.599999999999998979 ) ) ;
#1930=ADVANCED_FACE ( 'NONE', ( #16604 ), #9038, .T. ) ;
#1968=B_SPLINE_CURVE_WITH_KNOTS ( 'NONE', 3,
 ( #16333, #16580, #15212, #2528, #8055, #8236, #6868, #6693 ),
 .UNSPECIFIED., .F., .F.,
 ( 4, 2, 2, 4 ),
 ( 0.000000000000000000, 0.002450665683189819262, 0.003675998524784728893, 0.004901331366379638524 ),
 .UNSPECIFIED. ) ;
#1975=CARTESIAN_POINT ( 'NONE',  ( -4.000000000000000000, -2.309401076758510918, -0.5000000000000000000 ) ) ;
#1979=CARTESIAN_POINT ( 'NONE',  ( 0.000000000000000000, 0.000000000000000000, 2.399999999999999467 ) ) ;
#1989=EDGE_CURVE ( 'NONE', #5981, #2327, #463, .T. ) ;
#1995=CIRCLE ( 'NONE', #508, 2.500000000000000888 ) ;
#1999=CARTESIAN_POINT ( 'NONE',  ( -7.511572993685817836E-16, -4.618802153517020059, -4.700000000000000178 ) ) ;
#2003=CIRCLE ( 'NONE', #14450, 5.384454397937117776 ) ;
#2005=CARTESIAN_POINT ( 'NONE',  ( -1.393927851585477828, 4.043713361053527855, -3.226374918436836658 ) ) ;
#2013=CARTESIAN_POINT ( 'NONE',  ( 2.855764796983343068, -2.970025579236426516, -0.09382832055446284347 ) ) ;
#2015=AXIS2_PLACEMENT_3D ( 'NONE', #16835, #9642, #234 ) ;
#2020=VERTEX_POINT ( 'NONE', #15506 ) ;
#2037=ORIENTED_EDGE ( 'NONE', *, *, #5868, .T. ) ;
#2041=ORIENTED_EDGE ( 'NONE', *, *, #11253, .F. ) ;
#2043=CIRCLE ( 'NONE', #14497, 3.000000000000000000 ) ;
#2049=EDGE_CURVE ( 'NONE', #10575, #16479, #17270, .T. ) ;
#2061=APPLICATION_CONTEXT ( 'automotive_design' ) ;
#2062=CIRCLE ( 'NONE', #8124, 3.999999999999998224 ) ;
#2068=CARTESIAN_POINT ( 'NONE',  ( -4.154094228333753414, -2.398367420967510988, -3.421909803043223341 ) ) ;
#2097=CARTESIAN_POINT ( 'NONE',  ( 2.864813309430322025E-13, -4.796980096169637164, -3.421999068284422130 ) ) ;
#2110=DIRECTION ( 'NONE',  ( 0.000000000000000000, 0.000000000000000000, -1.000000000000000000 ) ) ;
#2113=ORIENTED_EDGE ( 'NONE', *, *, #1989, .T. ) ;
#2130=CARTESIAN_POINT ( 'NONE',  ( 2.756166666307278135, 3.027528586793024612, -2.923144239647247122 ) ) ;
#2137=CARTESIAN_POINT ( 'NONE',  ( 2.000000000000006217, 3.464101615137751722, -1.401678602859870442E-15 ) ) ;
#2138=CARTESIAN_POINT ( 'NONE',  ( -2.000000000000005329, -3.464101615137750390, 0.000000000000000000 ) ) ;
#2154=CARTESIAN_POINT ( 'NONE',  ( 2.100000000000000089, 0.000000000000000000, -4.394516984716110741 ) ) ;
#2181=B_SPLINE_CURVE_WITH_KNOTS ( 'NONE', 3,
 ( #758, #8747, #3477, #11437, #8919, #4651 ),
 .UNSPECIFIED., .F., .F.,
 ( 4, 2, 4 ),
 ( -3.640115492409826693E-06, 0.0002066546034006530282, 0.0004169493222937159212 ),
 .UNSPECIFIED. ) ;
#2186=FACE_OUTER_BOUND ( 'NONE', #6238, .T. ) ;
#2217=CARTESIAN_POINT ( 'NONE',  ( 3.472352378023213504, 2.614038573344063199, -3.020318136128407271 ) ) ;
#2225=EDGE_CURVE ( 'NONE', #7023, #8221, #11865, .T. ) ;
#2246=CARTESIAN_POINT ( 'NONE',  ( -3.679171394226034231, -2.494631558665840299, -0.3503314178412554880 ) ) ;
#2254=CARTESIAN_POINT ( 'NONE',  ( -1.360615521533533379, 4.061278559078136396, -3.205052026701836532 ) ) ;
#2275=CARTESIAN_POINT ( 'NONE',  ( 8.409399735147211686E-16, 4.618802153517009401, -4.700000000000000178 ) ) ;
#2284=CARTESIAN_POINT ( 'NONE',  ( 0.000000000000000000, 0.000000000000000000, 0.000000000000000000 ) ) ;
#2285=MECHANICAL_DESIGN_GEOMETRIC_PRESENTATION_REPRESENTATION('',(#17928),#1396);
#2287=VECTOR ( 'NONE', #16653, 1000.000000000000000 ) ;
#2301=EDGE_CURVE ( 'NONE', #2020, #7100, #4116, .T. ) ;
#2327=VERTEX_POINT ( 'NONE', #1435 ) ;
#2339=ORIENTED_EDGE ( 'NONE', *, *, #4394, .T. ) ;
#2354=AXIS2_PLACEMENT_3D ( 'NONE', #15166, #4012, #1213 ) ;
#2355=ORIENTED_EDGE ( 'NONE', *, *, #14140, .F. ) ;
#2390=CARTESIAN_POINT ( 'NONE',  ( 3.522881874163251492, -2.820349071480749537, -3.298443181295994009 ) ) ;
#2427=ADVANCED_FACE ( 'NONE', ( #16579 ), #12226, .T. ) ;
#2439=EDGE_LOOP ( 'NONE', ( #16960, #1721, #17284, #3294 ) ) ;
#2466=DIRECTION ( 'NONE',  ( 1.000000000000000000, 0.000000000000000000, 0.000000000000000000 ) ) ;
#2483=DIRECTION ( 'NONE',  ( -0.7071067811865489050, 8.659560562354950115E-17, 0.7071067811865462405 ) ) ;
#2528=CARTESIAN_POINT ( 'NONE',  ( 1.747541505913277948, -3.837784562140266864, -3.203702292528911144 ) ) ;
#2534=EDGE_CURVE ( 'NONE', #9939, #10468, #10447, .T. ) ;
#2536=CARTESIAN_POINT ( 'NONE',  ( -3.000000000000000000, 3.673940397442059868E-16, 2.399999999999999467 ) ) ;
#2537=B_SPLINE_CURVE_WITH_KNOTS ( 'NONE', 3,
 ( #10607, #3656, #9261, #14806, #16264, #3836, #1106, #2557 ),
 .UNSPECIFIED., .F., .F.,
 ( 4, 2, 2, 4 ),
 ( 2.465131517092369892E-07, 0.001183067374689850647, 0.001774477805458921347, 0.002365888236227992047 ),
 .UNSPECIFIED. ) ;
#2541=AXIS2_PLACEMENT_3D ( 'NONE', #14177, #10351, #17285 ) ;
#2551=ORIENTED_EDGE ( 'NONE', *, *, #6329, .T. ) ;
#2556=CARTESIAN_POINT ( 'NONE',  ( 0.000000000000000000, 0.000000000000000000, 0.000000000000000000 ) ) ;
#2557=CARTESIAN_POINT ( 'NONE',  ( 2.000000000000006217, 3.464101615137751722, -1.401678602859870442E-15 ) ) ;
#2564=ADVANCED_FACE ( 'NONE', ( #3737 ), #2962, .T. ) ;
#2571=EDGE_LOOP ( 'NONE', ( #10653, #1537, #14301, #6626 ) ) ;
#2586=ORIENTED_EDGE ( 'NONE', *, *, #9191, .T. ) ;
#2587=AXIS2_PLACEMENT_3D ( 'NONE', #7356, #12872, #11487 ) ;
#2604=ORIENTED_EDGE ( 'NONE', *, *, #15533, .F. ) ;
#2605=ORIENTED_EDGE ( 'NONE', *, *, #6651, .F. ) ;
#2610=ORIENTED_EDGE ( 'NONE', *, *, #4394, .F. ) ;
#2620=B_SPLINE_CURVE_WITH_KNOTS ( 'NONE', 3,
 ( #11816, #17395, #9022, #10275, #3667, #14650, #12000, #768 ),
 .UNSPECIFIED., .F., .F.,
 ( 4, 2, 2, 4 ),
 ( 0.000000000000000000, 0.002450665683189819262, 0.003675998524784728893, 0.004901331366379638524 ),
 .UNSPECIFIED. ) ;
#2642=CONICAL_SURFACE ( 'NONE', #7278, 3.999999999999998224, 0.8911886515913775009 ) ;
#2666=CARTESIAN_POINT ( 'NONE',  ( 4.000000000000000000, -0.8577736050348414576, -3.133260139357120888 ) ) ;
#2670=ADVANCED_FACE ( 'NONE', ( #3837 ), #994, .F. ) ;
#2674=CARTESIAN_POINT ( 'NONE',  ( -4.197393957002304887, 0.4069871074557444013, -3.203767560748928211 ) ) ;
#2681=DIRECTION ( 'NONE',  ( 0.000000000000000000, 0.000000000000000000, -1.000000000000000000 ) ) ;
#2731=DIRECTION ( 'NONE',  ( 1.000000000000000000, 0.000000000000000000, 0.000000000000000000 ) ) ;
#2737=DIRECTION ( 'NONE',  ( 1.000000000000000000, 0.000000000000000000, 0.000000000000000000 ) ) ;
#2739=B_SPLINE_CURVE_WITH_KNOTS ( 'NONE', 3,
 ( #10555, #2068, #17409, #12011, #16120, #3680 ),
 .UNSPECIFIED., .F., .F.,
 ( 4, 2, 4 ),
 ( -3.640115492410573777E-06, 0.0002066546034006518627, 0.0004169493222937142949 ),
 .UNSPECIFIED. ) ;
#2773=CARTESIAN_POINT ( 'NONE',  ( -4.141042022537586575, 2.227970427079376758, -3.387027626239164313 ) ) ;
#2799=ORIENTED_EDGE ( 'NONE', *, *, #11369, .T. ) ;
#2817=CARTESIAN_POINT ( 'NONE',  ( -0.02511946470933618461, 4.877415451931360835, -3.451298686683626826 ) ) ;
#2833=CARTESIAN_POINT ( 'NONE',  ( 2.000000000000006217, 3.464101615137751722, -1.401678602859870442E-15 ) ) ;
#2840=AXIS2_PLACEMENT_3D ( 'NONE', #10627, #5283, #6394 ) ;
#2848=EDGE_CURVE ( 'NONE', #3354, #5056, #4954, .T. ) ;
#2856=FACE_OUTER_BOUND ( 'NONE', #10015, .T. ) ;
#2877=FACE_OUTER_BOUND ( 'NONE', #11593, .T. ) ;
#2889=VERTEX_POINT ( 'NONE', #3617 ) ;
#2917=EDGE_CURVE ( 'NONE', #12636, #9205, #9827, .T. ) ;
#2941=AXIS2_PLACEMENT_3D ( 'NONE', #3142, #3328, #243 ) ;
#2962=TOROIDAL_SURFACE ( 'NONE', #13102, 3.199999999999998845, 0.8000000000000001554 ) ;
#2971=EDGE_LOOP ( 'NONE', ( #2037, #12866, #12964, #9958 ) ) ;
#3002=DIRECTION ( 'NONE',  ( 0.000000000000000000, 0.000000000000000000, 1.000000000000000000 ) ) ;
#3015=ORIENTED_EDGE ( 'NONE', *, *, #13337, .F. ) ;
#3020=ORIENTED_EDGE ( 'NONE', *, *, #13579, .F. ) ;
#3064=CARTESIAN_POINT ( 'NONE',  ( 1.243649364574536075E-15, 4.862606272033089816, -3.445885042887437244 ) ) ;
#3134=CARTESIAN_POINT ( 'NONE',  ( 3.199999999999998845, 0.000000000000000000, 1.599999999999999423 ) ) ;
#3142=CARTESIAN_POINT ( 'NONE',  ( 5.384454397937117776, 0.000000000000000000, -4.184454397937119374 ) ) ;
#3164=CARTESIAN_POINT ( 'NONE',  ( 5.384454397937117776, 0.000000000000000000, -4.700000000000000178 ) ) ;
#3167=CARTESIAN_POINT ( 'NONE',  ( -3.680118525130244400, 2.494084732383329062, -0.3507732604232482454 ) ) ;
#3210=ORIENTED_EDGE ( 'NONE', *, *, #6008, .T. ) ;
#3223=AXIS2_PLACEMENT_3D ( 'NONE', #9509, #15053, #6709 ) ;
#3228=EDGE_CURVE ( 'NONE', #9477, #16479, #8486, .T. ) ;
#3243=CARTESIAN_POINT ( 'NONE',  ( 4.000000000000000000, -6.071532165918824830E-15, -2.842992957459234749 ) ) ;
#3257=EDGE_LOOP ( 'NONE', ( #17364, #11314 ) ) ;
#3266=CARTESIAN_POINT ( 'NONE',  ( -3.355112389629168579, 2.681727112203154295, -0.2256878752776713681 ) ) ;
#3269=AXIS2_PLACEMENT_3D ( 'NONE', #1979, #6133, #442 ) ;
#3271=CARTESIAN_POINT ( 'NONE',  ( 1.317756351988340180, -3.857995168970211441, -0.04852650426602252154 ) ) ;
#3279=CARTESIAN_POINT ( 'NONE',  ( 3.680118525130243512, -2.494084732383340608, -0.3507732604232518536 ) ) ;
#3280=VECTOR ( 'NONE', #6407, 1000.000000000000000 ) ;
#3289=DIRECTION ( 'NONE',  ( 1.000000000000000000, 0.000000000000000000, 0.000000000000000000 ) ) ;
#3294=ORIENTED_EDGE ( 'NONE', *, *, #11753, .F. ) ;
#3324=ORIENTED_EDGE ( 'NONE', *, *, #9142, .F. ) ;
#3328=DIRECTION ( 'NONE',  ( 0.000000000000000000, -1.000000000000000000, 0.000000000000000000 ) ) ;
#3345=EDGE_CURVE ( 'NONE', #13298, #4903, #1397, .T. ) ;
#3354=VERTEX_POINT ( 'NONE', #2154 ) ;
#3380=DIRECTION ( 'NONE',  ( 0.000000000000000000, 0.000000000000000000, -1.000000000000000000 ) ) ;
#3428=VERTEX_POINT ( 'NONE', #13472 ) ;
#3433=LINE ( 'NONE', #9056, #10629 ) ;
#3442=ORIENTED_EDGE ( 'NONE', *, *, #7326, .T. ) ;
#3443=CARTESIAN_POINT ( 'NONE',  ( -2.805705207896067588, 3.226868319750155756, -3.203898532754366979 ) ) ;
#3449=EDGE_CURVE ( 'NONE', #8791, #13340, #10643, .T. ) ;
#3454=CARTESIAN_POINT ( 'NONE',  ( 0.000000000000000000, 0.000000000000000000, 1.159999999999999476 ) ) ;
#3477=CARTESIAN_POINT ( 'NONE',  ( -4.101948962585904468, 2.368261337751077722, -3.381124513963622569 ) ) ;
#3490=EDGE_CURVE ( 'NONE', #4413, #3428, #1995, .T. ) ;
#3527=SURFACE_SIDE_STYLE ('',( #6430 ) ) ;
#3569=AXIS2_PLACEMENT_3D ( 'NONE', #13910, #17859, #5649 ) ;
#3574=AXIS2_PLACEMENT_3D ( 'NONE', #13937, #4592, #7063 ) ;
#3575=AXIS2_PLACEMENT_3D ( 'NONE', #5095, #17575, #9272 ) ;
#3578=FACE_OUTER_BOUND ( 'NONE', #7252, .T. ) ;
#3580=CARTESIAN_POINT ( 'NONE',  ( -2.038300084272748336E-14, -4.618802153517010289, -0.5000000000000000000 ) ) ;
#3595=DIRECTION ( 'NONE',  ( -0.000000000000000000, -0.000000000000000000, 1.000000000000000000 ) ) ;
#3617=CARTESIAN_POINT ( 'NONE',  ( -4.000000000000000000, 2.309401076758501592, -0.4999999999999963363 ) ) ;
#3636=EDGE_CURVE ( 'NONE', #7716, #4413, #16915, .T. ) ;
#3641=CARTESIAN_POINT ( 'NONE',  ( 0.6666666666666659635, -4.233901974057268980, -3.000726591567087098 ) ) ;
#3644=CARTESIAN_POINT ( 'NONE',  ( 4.000000000000000000, 0.1981133338132479993, -1.407451120981426406E-15 ) ) ;
#3651=CARTESIAN_POINT ( 'NONE',  ( -4.000000000000000888, -1.539600717839008315, -3.000726591567082657 ) ) ;
#3656=CARTESIAN_POINT ( 'NONE',  ( 0.3198814748697599297, 4.434118497892178823, -0.3507732604232501328 ) ) ;
#3667=CARTESIAN_POINT ( 'NONE',  ( -2.804994570502171491, -3.229033611042460006, -3.226374918436839767 ) ) ;
#3680=CARTESIAN_POINT ( 'NONE',  ( -4.000000000000000000, -2.309401076758508253, -3.133295621305383083 ) ) ;
#3699=ORIENTED_EDGE ( 'NONE', *, *, #13392, .F. ) ;
#3705=FACE_OUTER_BOUND ( 'NONE', #14084, .T. ) ;
#3730=CARTESIAN_POINT ( 'NONE',  ( 0.6641139335921072417, -4.471067008846246971, -3.302142222889021372 ) ) ;
#3737=FACE_OUTER_BOUND ( 'NONE', #15811, .T. ) ;
#3745=ORIENTED_EDGE ( 'NONE', *, *, #3490, .T. ) ;
#3779=CARTESIAN_POINT ( 'NONE',  ( 4.211140560182196957, 2.431303136016537803, -3.445885042887434579 ) ) ;
#3792=CIRCLE ( 'NONE', #16255, 2.540000000000001368 ) ;
#3831=FACE_OUTER_BOUND ( 'NONE', #9072, .T. ) ;
#3836=CARTESIAN_POINT ( 'NONE',  ( 1.654252653721902444, 3.663718938583013340, -0.01223254789873544877 ) ) ;
#3837=FACE_OUTER_BOUND ( 'NONE', #14362, .T. ) ;
#3910=EDGE_CURVE ( 'NONE', #5051, #8513, #794, .T. ) ;
#3928=STYLED_ITEM ( 'NONE', ( #54 ), #7249 ) ;
#3951=CARTESIAN_POINT ( 'NONE',  ( -4.000000000000000000, -1.560351142792947732, -0.2242961665059824417 ) ) ;
#3955=VERTEX_POINT ( 'NONE', #14988 ) ;
#3972=( NAMED_UNIT ( * ) SI_UNIT ( $, .STERADIAN. ) SOLID_ANGLE_UNIT ( ) );
#4012=DIRECTION ( 'NONE',  ( -0.000000000000000000, -0.000000000000000000, 1.000000000000000000 ) ) ;
#4013=ORIENTED_EDGE ( 'NONE', *, *, #9997, .F. ) ;
#4045=ADVANCED_FACE ( 'NONE', ( #7845 ), #4829, .F. ) ;
#4050=ORIENTED_EDGE ( 'NONE', *, *, #11786, .T. ) ;
#4061=VERTEX_POINT ( 'NONE', #2833 ) ;
#4063=ADVANCED_FACE ( 'NONE', ( #9537 ), #16612, .F. ) ;
#4073=DIRECTION ( 'NONE',  ( -0.000000000000000000, -0.000000000000000000, -1.000000000000000000 ) ) ;
#4080=FACE_OUTER_BOUND ( 'NONE', #4673, .T. ) ;
#4082=CIRCLE ( 'NONE', #10723, 2.500000000000000888 ) ;
#4090=FACE_OUTER_BOUND ( 'NONE', #5029, .T. ) ;
#4095=CARTESIAN_POINT ( 'NONE',  ( -1.274241539467094064, -3.883118457693087500, -2.920601398289341954 ) ) ;
#4114=CARTESIAN_POINT ( 'NONE',  ( 4.000000000000000000, 2.472263363263126124, -3.387027814857423991 ) ) ;
#4116=CIRCLE ( 'NONE', #5846, 0.8000000000000003775 ) ;
#4117=EDGE_LOOP ( 'NONE', ( #10813, #14996 ) ) ;
#4132=ADVANCED_FACE ( 'NONE', ( #12539 ), #1224, .F. ) ;
#4156=ORIENTED_EDGE ( 'NONE', *, *, #15646, .F. ) ;
#4164=DIRECTION ( 'NONE',  ( -1.000000000000000000, 1.224646799147352714E-16, 0.000000000000000000 ) ) ;
#4189=CARTESIAN_POINT ( 'NONE',  ( -2.742797192660360484, -3.035247456001994859, -3.133250573521795257 ) ) ;
#4198=ORIENTED_EDGE ( 'NONE', *, *, #8588, .T. ) ;
#4204=CARTESIAN_POINT ( 'NONE',  ( 0.000000000000000000, 0.000000000000000000, 0.000000000000000000 ) ) ;
#4222=CARTESIAN_POINT ( 'NONE',  ( 0.000000000000000000, 0.000000000000000000, -3.700000000000000178 ) ) ;
#4230=B_SPLINE_CURVE_WITH_KNOTS ( 'NONE', 3,
 ( #1807, #11470, #3243, #12662, #12855 ),
 .UNSPECIFIED., .F., .F.,
 ( 4, 1, 4 ),
 ( 0.000000000000000000, 0.002309401076758504923, 0.004618802153517009845 ),
 .UNSPECIFIED. ) ;
#4238=CARTESIAN_POINT ( 'NONE',  ( 2.540000000000001368, 0.000000000000000000, 1.599999999999998979 ) ) ;
#4240=DIRECTION ( 'NONE',  ( -0.000000000000000000, -0.000000000000000000, 1.000000000000000000 ) ) ;
#4242=LINE ( 'NONE', #10271, #13073 ) ;
#4261=PLANE ( 'NONE',  #853 ) ;
#4273=CARTESIAN_POINT ( 'NONE',  ( -0.1410420225375869918, 4.700232803196136011, -3.387027626239166089 ) ) ;
#4288=CARTESIAN_POINT ( 'NONE',  ( 4.000000000000000000, -0.8732118962410247986, -2.923153487222570401 ) ) ;
#4303=FACE_OUTER_BOUND ( 'NONE', #14284, .T. ) ;
#4313=ADVANCED_FACE ( 'NONE', ( #10256 ), #17916, .T. ) ;
#4332=LINE ( 'NONE', #9844, #14772 ) ;
#4357=LINE ( 'NONE', #9601, #10898 ) ;
#4360=CARTESIAN_POINT ( 'NONE',  ( -5.560781378645573980, 0.000000000000000000, -3.700000000000000178 ) ) ;
#4375=VERTEX_POINT ( 'NONE', #11783 ) ;
#4378=CARTESIAN_POINT ( 'NONE',  ( 4.000000000000000000, 1.658584703716865061, -3.231554742509319844 ) ) ;
#4391=EDGE_LOOP ( 'NONE', ( #11757, #4743, #516, #13221, #5306, #584 ) ) ;
#4394=EDGE_CURVE ( 'NONE', #3955, #16943, #17540, .T. ) ;
#4396=AXIS2_PLACEMENT_3D ( 'NONE', #13366, #16277, #6481 ) ;
#4413=VERTEX_POINT ( 'NONE', #4719 ) ;
#4420=FACE_OUTER_BOUND ( 'NONE', #893, .T. ) ;
#4442=CARTESIAN_POINT ( 'NONE',  ( -2.687328764639636880, 3.067272167851287534, -0.05923475698270543044 ) ) ;
#4450=DIRECTION ( 'NONE',  ( 0.7071067811865489050, 0.000000000000000000, 0.7071067811865462405 ) ) ;
#4460=ORIENTED_EDGE ( 'NONE', *, *, #9181, .F. ) ;
#4490=CARTESIAN_POINT ( 'NONE',  ( -4.197393957002304887, -0.8151795401431392030, -3.203767560748937537 ) ) ;
#4503=FACE_OUTER_BOUND ( 'NONE', #7765, .T. ) ;
#4506=CARTESIAN_POINT ( 'NONE',  ( 8.409399735147209713E-16, 4.618802153517009401, -3.204269196027528022 ) ) ;
#4507=FACE_BOUND ( 'NONE', #3257, .T. ) ;
#4510=CARTESIAN_POINT ( 'NONE',  ( -2.500000000000000888, 3.061616997868384127E-16, -25.03750572909317285 ) ) ;
#4516=EDGE_CURVE ( 'NONE', #16863, #16943, #3433, .T. ) ;
#4531=DIRECTION ( 'NONE',  ( 1.000000000000000000, 0.000000000000000000, 0.000000000000000000 ) ) ;
#4546=VECTOR ( 'NONE', #15808, 1000.000000000000000 ) ;
#4587=CARTESIAN_POINT ( 'NONE',  ( 3.999999999999998224, 0.000000000000000000, 0.000000000000000000 ) ) ;
#4589=CARTESIAN_POINT ( 'NONE',  ( -4.203934431905299363, -1.640681339110445114, -3.298434044919825503 ) ) ;
#4592=DIRECTION ( 'NONE',  ( 0.000000000000000000, 0.000000000000000000, -1.000000000000000000 ) ) ;
#4651=CARTESIAN_POINT ( 'NONE',  ( -4.000000000000000000, 2.309401076758501592, -3.133295621305381307 ) ) ;
#4673=EDGE_LOOP ( 'NONE', ( #241, #2605, #11554 ) ) ;
#4675=CARTESIAN_POINT ( 'NONE',  ( 0.000000000000000000, 0.000000000000000000, 0.000000000000000000 ) ) ;
#4680=CARTESIAN_POINT ( 'NONE',  ( -4.000000000000000000, -0.8232522521399842086, -3.130632262998158666 ) ) ;
#4681=CARTESIAN_POINT ( 'NONE',  ( 1.243649364574536075E-15, 4.862606272033089816, -3.445885042887437244 ) ) ;
#4686=CIRCLE ( 'NONE', #633, 3.999999999999998224 ) ;
#4690=ADVANCED_FACE ( 'NONE', ( #3578 ), #17647, .F. ) ;
#4713=DIRECTION ( 'NONE',  ( -0.000000000000000000, -0.000000000000000000, 1.000000000000000000 ) ) ;
#4719=CARTESIAN_POINT ( 'NONE',  ( -2.500000000000000888, 0.000000000000000000, -4.674599999999997202 ) ) ;
#4743=ORIENTED_EDGE ( 'NONE', *, *, #9181, .T. ) ;
#4753=EDGE_CURVE ( 'NONE', #6357, #4375, #2181, .T. ) ;
#4764=CARTESIAN_POINT ( 'NONE',  ( 4.000000000000000000, -0.3979232138631215721, -1.387439967602543955E-15 ) ) ;
#4768=CARTESIAN_POINT ( 'NONE',  ( 3.510273485745309507, 2.827716139362654424, -3.310536846335887962 ) ) ;
#4774=SURFACE_STYLE_FILL_AREA ( #17235 ) ;
#4782=( GEOMETRIC_REPRESENTATION_CONTEXT ( 3 ) GLOBAL_UNCERTAINTY_ASSIGNED_CONTEXT ( ( #8291 ) ) GLOBAL_UNIT_ASSIGNED_CONTEXT ( ( #9216, #11751, #10645 ) ) REPRESENTATION_CONTEXT ( 'NONE', 'WORKASPACE' ) );
#4787=FACE_OUTER_BOUND ( 'NONE', #5956, .T. ) ;
#4826=CYLINDRICAL_SURFACE ( 'NONE', #648, 4.000000000000000000 ) ;
#4829=CONICAL_SURFACE ( 'NONE', #6289, 2.500000000000000888, 0.9599310885968781459 ) ;
#4834=CARTESIAN_POINT ( 'NONE',  ( -3.000000000000000000, 3.673940397442059868E-16, 1.599999999999998979 ) ) ;
#4858=CARTESIAN_POINT ( 'NONE',  ( 4.203833317240879275, 1.627343821129583867, -3.297273115243890995 ) ) ;
#4868=ORIENTED_EDGE ( 'NONE', *, *, #10123, .F. ) ;
#4892=CIRCLE ( 'NONE', #2015, 2.100000000000000089 ) ;
#4903=VERTEX_POINT ( 'NONE', #16685 ) ;
#4930=CARTESIAN_POINT ( 'NONE',  ( 0.000000000000000000, 0.000000000000000000, -4.184454397937119374 ) ) ;
#4947=CARTESIAN_POINT ( 'NONE',  ( -0.6666666666666659635, 4.233901974057258322, -3.000726591567082657 ) ) ;
#4950=CARTESIAN_POINT ( 'NONE',  ( -0.6641139335927965792, 4.471067008845558632, -3.302142222888768686 ) ) ;
#4954=LINE ( 'NONE', #11313, #16457 ) ;
#4960=ORIENTED_EDGE ( 'NONE', *, *, #16415, .F. ) ;
#4972=CARTESIAN_POINT ( 'NONE',  ( -5.816800114226745675E-16, -4.862606272033100474, -3.445885042887441241 ) ) ;
#4987=CARTESIAN_POINT ( 'NONE',  ( 3.999999999999998224, 0.000000000000000000, 0.000000000000000000 ) ) ;
#4999=B_SPLINE_CURVE_WITH_KNOTS ( 'NONE', 3,
 ( #12970, #3641, #816, #11780, #6348 ),
 .UNSPECIFIED., .F., .F.,
 ( 4, 1, 4 ),
 ( 4.386880129527780036E-20, 0.002309401076758504055, 0.004618802153517008978 ),
 .UNSPECIFIED. ) ;
#5010=CARTESIAN_POINT ( 'NONE',  ( -0.6448876103708482965, -4.246476118072356698, -0.2256878752776764752 ) ) ;
#5014=CARTESIAN_POINT ( 'NONE',  ( 0.000000000000000000, 0.000000000000000000, 13.31572692736085095 ) ) ;
#5022=CARTESIAN_POINT ( 'NONE',  ( 0.000000000000000000, 0.000000000000000000, -4.699999999999999289 ) ) ;
#5029=EDGE_LOOP ( 'NONE', ( #14424, #10557, #1479, #4868 ) ) ;
#5041=CARTESIAN_POINT ( 'NONE',  ( -2.712778981739305095, 3.052578478157828012, -3.130620751972063687 ) ) ;
#5045=DIRECTION ( 'NONE',  ( 0.8660254037844378194, -0.5000000000000014433, 0.000000000000000000 ) ) ;
#5051=VERTEX_POINT ( 'NONE', #11202 ) ;
#5054=B_SPLINE_CURVE_WITH_KNOTS ( 'NONE', 3,
 ( #96, #3167, #3266, #5964, #4442, #9953, #1642, #9763 ),
 .UNSPECIFIED., .F., .F.,
 ( 4, 2, 2, 4 ),
 ( 2.465131517071352357E-07, 0.001183067374689843057, 0.001774477805458910939, 0.002365888236227979037 ),
 .UNSPECIFIED. ) ;
#5056=VERTEX_POINT ( 'NONE', #8517 ) ;
#5073=CARTESIAN_POINT ( 'NONE',  ( 3.999999999999999112, 1.563622288139204342, -0.2253451193528351326 ) ) ;
#5083=CARTESIAN_POINT ( 'NONE',  ( 0.6666666666666668517, 4.233901974057260986, -3.000726591567082657 ) ) ;
#5087=CARTESIAN_POINT ( 'NONE',  ( 0.000000000000000000, 0.000000000000000000, 1.599999999999999423 ) ) ;
#5095=CARTESIAN_POINT ( 'NONE',  ( 0.000000000000000000, 0.000000000000000000, 0.000000000000000000 ) ) ;
#5112=LINE ( 'NONE', #10554, #14203 ) ;
#5133=ORIENTED_EDGE ( 'NONE', *, *, #13337, .T. ) ;
#5151=ORIENTED_EDGE ( 'NONE', *, *, #16415, .T. ) ;
#5165=CARTESIAN_POINT ( 'NONE',  ( 2.712778981737816508, -3.052578478158503028, -3.130620751971882054 ) ) ;
#5186=CARTESIAN_POINT ( 'NONE',  ( 4.211140560182196957, 2.431303136016537803, -3.445885042887434579 ) ) ;
#5269=DIRECTION ( 'NONE',  ( 1.000000000000000000, 0.000000000000000000, 0.000000000000000000 ) ) ;
#5281=DIRECTION ( 'NONE',  ( -0.000000000000000000, -0.000000000000000000, -1.000000000000000000 ) ) ;
#5283=DIRECTION ( 'NONE',  ( -0.000000000000000000, -0.000000000000000000, 1.000000000000000000 ) ) ;
#5291=LINE ( 'NONE', #16122, #3280 ) ;
#5301=ORIENTED_EDGE ( 'NONE', *, *, #11786, .F. ) ;
#5303=DIRECTION ( 'NONE',  ( 1.000000000000000000, 0.000000000000000000, 0.000000000000000000 ) ) ;
#5306=ORIENTED_EDGE ( 'NONE', *, *, #12713, .T. ) ;
#5321=DIRECTION ( 'NONE',  ( -0.8660254037844381525, -0.5000000000000007772, 0.000000000000000000 ) ) ;
#5339=B_SPLINE_CURVE_WITH_KNOTS ( 'NONE', 3,
 ( #17440, #14419, #11957, #15778, #2097, #4972 ),
 .UNSPECIFIED., .F., .F.,
 ( 4, 2, 4 ),
 ( 0.000000000000000000, 0.0002095117440854745035, 0.0004190234881709490071 ),
 .UNSPECIFIED. ) ;
#5346=CARTESIAN_POINT ( 'NONE',  ( 0.6810530063609926410, 4.461079733298231709, -3.298443181296264459 ) ) ;
#5349=MANIFOLD_SOLID_BREP ( 'TorqueElement', #17724 ) ;
#5354=COLOUR_RGB ( '', 0.66274510, 0.83137255, 0.94901961) ;
#5361=ORIENTED_EDGE ( 'NONE', *, *, #1378, .T. ) ;
#5364=CARTESIAN_POINT ( 'NONE',  ( 3.999999999999999556, 0.8228621380349563363, -3.130611579770401498 ) ) ;
#5375=ORIENTED_EDGE ( 'NONE', *, *, #14298, .F. ) ;
#5416=ORIENTED_EDGE ( 'NONE', *, *, #2049, .T. ) ;
#5425=DIRECTION ( 'NONE',  ( -0.8660254037844378194, 0.5000000000000014433, 0.000000000000000000 ) ) ;
#5429=CARTESIAN_POINT ( 'NONE',  ( 1.243649364574536075E-15, 4.862606272033089816, -3.445885042887437244 ) ) ;
#5432=COLOUR_RGB ( '', 0.66274510, 0.83137255, 0.94901961) ;
#5446=CARTESIAN_POINT ( 'NONE',  ( -3.333333333333332149, -2.694301256218260665, -3.000726591567082657 ) ) ;
#5461=CARTESIAN_POINT ( 'NONE',  ( -4.197393957002304887, -7.639915766855272736E-14, -3.203767560748932208 ) ) ;
#5467=ORIENTED_EDGE ( 'NONE', *, *, #15948, .T. ) ;
#5469=B_SPLINE_CURVE_WITH_KNOTS ( 'NONE', 3,
 ( #7553, #7649, #12899, #302, #11332, #483 ),
 .UNSPECIFIED., .F., .F.,
 ( 4, 2, 4 ),
 ( 0.002365888236227979037, 0.003551327329835078910, 0.004736766423442178783 ),
 .UNSPECIFIED. ) ;
#5478=DIRECTION ( 'NONE',  ( 1.000000000000000000, 0.000000000000000000, 0.000000000000000000 ) ) ;
#5499=VERTEX_POINT ( 'NONE', #4238 ) ;
#5515=CARTESIAN_POINT ( 'NONE',  ( 4.000000000000000000, 2.309401076758498483, -4.700000000000000178 ) ) ;
#5531=EDGE_LOOP ( 'NONE', ( #15489, #14823 ) ) ;
#5563=CARTESIAN_POINT ( 'NONE',  ( -4.000000000000000000, -0.3979232138631214610, -1.402686560653121361E-15 ) ) ;
#5606=CIRCLE ( 'NONE', #7097, 3.000000000000000000 ) ;
#5617=ORIENTED_EDGE ( 'NONE', *, *, #2301, .F. ) ;
#5630=CARTESIAN_POINT ( 'NONE',  ( 4.000000000000000000, 0.8378468363844291389, -2.920592527564379370 ) ) ;
#5649=DIRECTION ( 'NONE',  ( 1.000000000000000000, 0.000000000000000000, 0.000000000000000000 ) ) ;
#5700=CARTESIAN_POINT ( 'NONE',  ( 4.197393957002304887, -0.4069871074557454560, -3.203767560748928211 ) ) ;
#5702=EDGE_CURVE ( 'NONE', #9563, #12636, #6031, .T. ) ;
#5723=B_SPLINE_CURVE_WITH_KNOTS ( 'NONE', 3,
 ( #7440, #11684, #3443, #13146, #2005, #7530, #7009, #8973 ),
 .UNSPECIFIED., .F., .F.,
 ( 4, 2, 2, 4 ),
 ( 0.000000000000000000, 0.002450665683189818395, 0.003675998524784727592, 0.004901331366379636789 ),
 .UNSPECIFIED. ) ;
#5729=ADVANCED_FACE ( 'NONE', ( #14673 ), #8420, .F. ) ;
#5737=ORIENTED_EDGE ( 'NONE', *, *, #6008, .F. ) ;
#5752=ORIENTED_EDGE ( 'NONE', *, *, #13314, .T. ) ;
#5754=CARTESIAN_POINT ( 'NONE',  ( -4.197393957002304887, -7.639915766855272736E-14, -3.203767560748932208 ) ) ;
#5761=EDGE_CURVE ( 'NONE', #12543, #364, #8438, .T. ) ;
#5764=CIRCLE ( 'NONE', #15923, 3.999999999999998224 ) ;
#5834=CARTESIAN_POINT ( 'NONE',  ( -4.000000000000000000, 0.7924765000094609046, -0.05906175389889908173 ) ) ;
#5846=AXIS2_PLACEMENT_3D ( 'NONE', #15033, #15210, #4164 ) ;
#5853=CARTESIAN_POINT ( 'NONE',  ( -4.000000000000000000, 2.471529427528105227, -3.386887593711408240 ) ) ;
#5868=EDGE_CURVE ( 'NONE', #7716, #3354, #831, .T. ) ;
#5869=TOROIDAL_SURFACE ( 'NONE', #16039, 3.199999999999998845, 0.8000000000000001554 ) ;
#5883=CARTESIAN_POINT ( 'NONE',  ( 0.6507732100473438974, -4.243078065514786168, -0.2236248678334921414 ) ) ;
#5956=EDGE_LOOP ( 'NONE', ( #2610, #8390, #11440, #4198, #12672 ) ) ;
#5964=CARTESIAN_POINT ( 'NONE',  ( -2.855764796983341736, 2.970025579236416302, -0.09382832055445670949 ) ) ;
#5969=ADVANCED_FACE ( 'NONE', ( #4090 ), #16783, .F. ) ;
#5970=DIRECTION ( 'NONE',  ( -0.000000000000000000, -0.000000000000000000, 1.000000000000000000 ) ) ;
#5981=VERTEX_POINT ( 'NONE', #16515 ) ;
#5985=PRODUCT_DEFINITION_FORMATION_WITH_SPECIFIED_SOURCE ( 'ANY', '', #15045, .NOT_KNOWN. ) ;
#5999=AXIS2_PLACEMENT_3D ( 'NONE', #15806, #3380, #8988 ) ;
#6008=EDGE_CURVE ( 'NONE', #16863, #11660, #16021, .T. ) ;
#6031=B_SPLINE_CURVE_WITH_KNOTS ( 'NONE', 3,
 ( #3779, #4858, #15941, #17603 ),
 .UNSPECIFIED., .F., .F.,
 ( 4, 4 ),
 ( 0.000000000000000000, 0.002452478801916362864 ),
 .UNSPECIFIED. ) ;
#6077=CARTESIAN_POINT ( 'NONE',  ( 4.000000000000000000, 2.309401076758510918, -0.5000000000000000000 ) ) ;
#6086=ORIENTED_EDGE ( 'NONE', *, *, #9838, .T. ) ;
#6098=VECTOR ( 'NONE', #7793, 1000.000000000000000 ) ;
#6128=EDGE_LOOP ( 'NONE', ( #16808, #4013, #694 ) ) ;
#6132=CARTESIAN_POINT ( 'NONE',  ( -4.211399291375529153, 2.459730787265042462, -3.451162385478148131 ) ) ;
#6133=DIRECTION ( 'NONE',  ( -0.000000000000000000, -0.000000000000000000, 1.000000000000000000 ) ) ;
#6135=CARTESIAN_POINT ( 'NONE',  ( -1.999999999999999556, 3.464101615137755719, -2.842992957459236525 ) ) ;
#6138=CARTESIAN_POINT ( 'NONE',  ( -1.243833333691421572, 3.900674643483235560, -2.923144239647432752 ) ) ;
#6148=EDGE_CURVE ( 'NONE', #9205, #14231, #1968, .T. ) ;
#6151=ORIENTED_EDGE ( 'NONE', *, *, #6329, .F. ) ;
#6166=EDGE_LOOP ( 'NONE', ( #308, #2339, #7470 ) ) ;
#6168=DIRECTION ( 'NONE',  ( 0.000000000000000000, 0.000000000000000000, 1.000000000000000000 ) ) ;
#6180=CARTESIAN_POINT ( 'NONE',  ( 0.000000000000000000, 0.000000000000000000, 0.000000000000000000 ) ) ;
#6196=ORIENTED_EDGE ( 'NONE', *, *, #17524, .F. ) ;
#6238=EDGE_LOOP ( 'NONE', ( #5752, #2113, #5133, #5416, #17891 ) ) ;
#6289=AXIS2_PLACEMENT_3D ( 'NONE', #1124, #8101, #16716 ) ;
#6310=EDGE_LOOP ( 'NONE', ( #10088, #13409, #13253, #6086, #11876, #12705, #6860 ) ) ;
#6318=CARTESIAN_POINT ( 'NONE',  ( -0.5469803261936758698, 4.303002914946057800, -3.235259548912099881 ) ) ;
#6329=EDGE_CURVE ( 'NONE', #11222, #6357, #1510, .T. ) ;
#6339=AXIS2_PLACEMENT_3D ( 'NONE', #15041, #9581, #6611 ) ;
#6348=CARTESIAN_POINT ( 'NONE',  ( 4.000000000000000000, -2.309401076758510918, -3.133295621305383083 ) ) ;
#6357=VERTEX_POINT ( 'NONE', #6835 ) ;
#6361=CARTESIAN_POINT ( 'NONE',  ( -3.999999999999999112, 1.539600717838999877, -3.000726591567080881 ) ) ;
#6368=CARTESIAN_POINT ( 'NONE',  ( 4.235887314095728939, 2.417314327725964773, -3.451162025751985496 ) ) ;
#6377=CARTESIAN_POINT ( 'NONE',  ( -1.828356344711642878, -3.563200125723190670, -8.309957901196191823E-15 ) ) ;
#6394=DIRECTION ( 'NONE',  ( 1.000000000000000000, 0.000000000000000000, 0.000000000000000000 ) ) ;
#6407=DIRECTION ( 'NONE',  ( -0.000000000000000000, -0.000000000000000000, 1.000000000000000000 ) ) ;
#6430=SURFACE_STYLE_FILL_AREA ( #15958 ) ;
#6476=ORIENTED_EDGE ( 'NONE', *, *, #16868, .F. ) ;
#6481=DIRECTION ( 'NONE',  ( 1.000000000000000000, 0.000000000000000000, 0.000000000000000000 ) ) ;
#6496=CARTESIAN_POINT ( 'NONE',  ( 5.560781378645573980, 6.809993116116507654E-16, -3.700000000000000178 ) ) ;
#6532=ORIENTED_EDGE ( 'NONE', *, *, #1518, .F. ) ;
#6549=CARTESIAN_POINT ( 'NONE',  ( -2.836862643238851511, -3.208966885971353822, -3.205052026701894707 ) ) ;
#6555=CARTESIAN_POINT ( 'NONE',  ( -3.000000000000000000, 3.673940397442059868E-16, 13.31572692736085095 ) ) ;
#6562=CARTESIAN_POINT ( 'NONE',  ( 3.035766082959412415E-15, 4.618802153517010289, -0.5000000000000000000 ) ) ;
#6567=ORIENTED_EDGE ( 'NONE', *, *, #13235, .F. ) ;
#6585=CARTESIAN_POINT ( 'NONE',  ( 0.000000000000000000, 0.000000000000000000, -25.03750572909317285 ) ) ;
#6611=DIRECTION ( 'NONE',  ( 1.000000000000000000, 0.000000000000000000, 0.000000000000000000 ) ) ;
#6626=ORIENTED_EDGE ( 'NONE', *, *, #13579, .T. ) ;
#6632=VECTOR ( 'NONE', #11908, 1000.000000000000000 ) ;
#6637=EDGE_LOOP ( 'NONE', ( #10350, #6947, #13950, #4960, #7055 ) ) ;
#6651=EDGE_CURVE ( 'NONE', #16479, #7462, #13929, .T. ) ;
#6666=CIRCLE ( 'NONE', #2354, 3.000000000000000000 ) ;
#6693=CARTESIAN_POINT ( 'NONE',  ( -5.816800114226745675E-16, -4.862606272033100474, -3.445885042887441241 ) ) ;
#6709=DIRECTION ( 'NONE',  ( -1.000000000000000000, 0.000000000000000000, 0.000000000000000000 ) ) ;
#6724=VECTOR ( 'NONE', #8888, 1000.000000000000000 ) ;
#6740=CARTESIAN_POINT ( 'NONE',  ( 0.000000000000000000, 0.000000000000000000, -25.03750572909317285 ) ) ;
#6756=ORIENTED_EDGE ( 'NONE', *, *, #14708, .F. ) ;
#6780=ADVANCED_FACE ( 'NONE', ( #9506 ), #4261, .T. ) ;
#6796=CARTESIAN_POINT ( 'NONE',  ( 0.000000000000000000, 0.000000000000000000, -4.699999999999999289 ) ) ;
#6805=DIRECTION ( 'NONE',  ( -0.000000000000000000, -0.000000000000000000, 1.000000000000000000 ) ) ;
#6819=ORIENTED_EDGE ( 'NONE', *, *, #8675, .T. ) ;
#6830=CARTESIAN_POINT ( 'NONE',  ( 4.000000000000000000, -2.471526491860382091, -3.386887032901836125 ) ) ;
#6835=CARTESIAN_POINT ( 'NONE',  ( -4.211140560182196957, 2.431303136016540911, -3.445885042887435468 ) ) ;
#6860=ORIENTED_EDGE ( 'NONE', *, *, #3449, .T. ) ;
#6864=EDGE_LOOP ( 'NONE', ( #5375, #1214, #10764 ) ) ;
#6868=CARTESIAN_POINT ( 'NONE',  ( 0.3461262719736145632, -4.658553426539295828, -3.371615880910378671 ) ) ;
#6875=ADVANCED_FACE ( 'NONE', ( #4787 ), #11401, .F. ) ;
#6904=CARTESIAN_POINT ( 'NONE',  ( 4.000000000000000000, 2.309401076758510918, -0.5000000000000000000 ) ) ;
#6909=ORIENTED_EDGE ( 'NONE', *, *, #6651, .T. ) ;
#6911=CARTESIAN_POINT ( 'NONE',  ( 4.024499207728657879, 2.323545700935572000, -3.272172305156507921 ) ) ;
#6925=ORIENTED_EDGE ( 'NONE', *, *, #15574, .T. ) ;
#6928=VERTEX_POINT ( 'NONE', #3164 ) ;
#6932=DIRECTION ( 'NONE',  ( -1.000000000000000000, 0.000000000000000000, 0.000000000000000000 ) ) ;
#6946=ADVANCED_FACE ( 'NONE', ( #7172, #10133 ), #271, .F. ) ;
#6947=ORIENTED_EDGE ( 'NONE', *, *, #2917, .F. ) ;
#6962=B_SPLINE_CURVE_WITH_KNOTS ( 'NONE', 3,
 ( #8001, #5446, #13717, #13540, #10873 ),
 .UNSPECIFIED., .F., .F.,
 ( 4, 1, 4 ),
 ( 0.000000000000000000, 0.002309401076758504923, 0.004618802153517009845 ),
 .UNSPECIFIED. ) ;
#7009=CARTESIAN_POINT ( 'NONE',  ( -0.3461262719736134530, 4.658553426539286946, -3.371615880910374674 ) ) ;
#7013=CARTESIAN_POINT ( 'NONE',  ( -7.999999999999991118, -1.301042606982605321E-15, -4.700000000000000178 ) ) ;
#7023=VERTEX_POINT ( 'NONE', #14858 ) ;
#7035=ADVANCED_FACE ( 'NONE', ( #3705 ), #14510, .F. ) ;
#7055=ORIENTED_EDGE ( 'NONE', *, *, #8588, .F. ) ;
#7063=DIRECTION ( 'NONE',  ( -1.000000000000000000, 0.000000000000000000, -0.000000000000000000 ) ) ;
#7087=CARTESIAN_POINT ( 'NONE',  ( 0.3208286057739613839, -4.433571671609690235, -0.3503314178412654245 ) ) ;
#7097=AXIS2_PLACEMENT_3D ( 'NONE', #10961, #16523, #5269 ) ;
#7100=VERTEX_POINT ( 'NONE', #8143 ) ;
#7149=CARTESIAN_POINT ( 'NONE',  ( -4.000000000000000000, 1.700072946616194569, -3.020308295356459727 ) ) ;
#7150=CARTESIAN_POINT ( 'NONE',  ( 4.211140560182196957, 2.431303136016537803, -3.445885042887434579 ) ) ;
#7158=VERTEX_POINT ( 'NONE', #13933 ) ;
#7168=B_SPLINE_CURVE_WITH_KNOTS ( 'NONE', 3,
 ( #7633, #3279, #17352, #2013, #10419, #14343, #13062, #11966 ),
 .UNSPECIFIED., .F., .F.,
 ( 4, 2, 2, 4 ),
 ( 2.465131517101105978E-07, 0.001183067374689841323, 0.001774477805458907036, 0.002365888236227972966 ),
 .UNSPECIFIED. ) ;
#7172=FACE_BOUND ( 'NONE', #13603, .T. ) ;
#7221=CARTESIAN_POINT ( 'NONE',  ( -3.999999999999998224, 0.000000000000000000, 0.000000000000000000 ) ) ;
#7236=CARTESIAN_POINT ( 'NONE',  ( 0.000000000000000000, 0.000000000000000000, 2.399999999999999467 ) ) ;
#7240=( BOUNDED_SURFACE ( )  B_SPLINE_SURFACE ( 3, 2, ( 
 ( #13168, #7816, #10430 ),
 ( #13346, #8995, #3730 ),
 ( #926, #9254, #9342 ),
 ( #17644, #5165, #10681 ),
 ( #7644, #1018, #2390 ),
 ( #16256, #17369, #658 ) ),
 .UNSPECIFIED., .F., .F., .T. ) 
 B_SPLINE_SURFACE_WITH_KNOTS ( ( 4, 2, 4 ),
 ( 3, 3 ),
 ( 0.02023740217035201183, 0.02269762987400600340, 0.02515785757765999150 ),
 ( 0.000000000000000000, 1.000000000000000000 ),
 .UNSPECIFIED. ) 
 GEOMETRIC_REPRESENTATION_ITEM ( )  RATIONAL_B_SPLINE_SURFACE ( (
 ( 1.000000000000000000, 0.8047781539129728046, 1.000000000000000000),
 ( 1.000000000000000000, 0.8123770319058200018, 1.000000000000000000),
 ( 1.000000000000000000, 0.8190663783055447400, 1.000000000000000000),
 ( 1.000000000000000000, 0.8192359702878471150, 1.000000000000000000),
 ( 1.000000000000000000, 0.8126134888418757862, 1.000000000000000000),
 ( 1.000000000000000000, 0.8047712368238109093, 1.000000000000000000) ) ) 
 REPRESENTATION_ITEM ( '' )  SURFACE ( )  );
#7249=ADVANCED_BREP_SHAPE_REPRESENTATION ( '', ( #5349, #3575 ), #4782 ) ;
#7252=EDGE_LOOP ( 'NONE', ( #6532, #3699, #300, #1694 ) ) ;
#7256=CARTESIAN_POINT ( 'NONE',  ( 4.000000000000000000, 2.309401076758498483, -4.700000000000000178 ) ) ;
#7278=AXIS2_PLACEMENT_3D ( 'NONE', #1065, #9647, #9728 ) ;
#7287=ORIENTED_EDGE ( 'NONE', *, *, #27, .T. ) ;
#7293=EDGE_CURVE ( 'NONE', #4903, #7100, #15945, .T. ) ;
#7311=ADVANCED_FACE ( 'NONE', ( #4503 ), #187, .F. ) ;
#7313=CARTESIAN_POINT ( 'NONE',  ( -4.000000000000000000, 1.941961291383474508, -0.3515519931180230984 ) ) ;
#7317=CARTESIAN_POINT ( 'NONE',  ( -4.211140560182196957, -2.431303136016548017, -3.445885042887436356 ) ) ;
#7326=EDGE_CURVE ( 'NONE', #13340, #8791, #16234, .T. ) ;
#7333=CARTESIAN_POINT ( 'NONE',  ( -4.000000000000000000, -2.472261030551091476, -3.387027369136294208 ) ) ;
#7343=ORIENTED_EDGE ( 'NONE', *, *, #17406, .T. ) ;
#7344=AXIS2_PLACEMENT_3D ( 'NONE', #4930, #3595, #9117 ) ;
#7356=CARTESIAN_POINT ( 'NONE',  ( 0.000000000000000000, 3.000000000000000000, 2.399999999999999467 ) ) ;
#7385=CARTESIAN_POINT ( 'NONE',  ( -2.540000000000001368, 3.110602869834278640E-16, 1.599999999999998979 ) ) ;
#7400=DIRECTION ( 'NONE',  ( 1.000000000000000000, 0.000000000000000000, 0.000000000000000000 ) ) ;
#7414=EDGE_LOOP ( 'NONE', ( #14521, #9054, #11237, #2041 ) ) ;
#7420=CARTESIAN_POINT ( 'NONE',  ( -4.000000000000000000, 0.8576023918602336815, -3.133238574225035933 ) ) ;
#7422=EDGE_CURVE ( 'NONE', #10468, #8221, #2043, .T. ) ;
#7440=CARTESIAN_POINT ( 'NONE',  ( -4.211140560182196957, 2.431303136016540911, -3.445885042887435468 ) ) ;
#7443=ORIENTED_EDGE ( 'NONE', *, *, #9142, .T. ) ;
#7446=DIRECTION ( 'NONE',  ( 1.000000000000000000, 0.000000000000000000, 0.000000000000000000 ) ) ;
#7448=CARTESIAN_POINT ( 'NONE',  ( 4.197393957002304887, 7.725818140447171444E-14, -3.203767560748932208 ) ) ;
#7462=VERTEX_POINT ( 'NONE', #13390 ) ;
#7470=ORIENTED_EDGE ( 'NONE', *, *, #11698, .F. ) ;
#7491=ORIENTED_EDGE ( 'NONE', *, *, #603, .F. ) ;
#7492=CIRCLE ( 'NONE', #14152, 5.384454397937117776 ) ;
#7501=CARTESIAN_POINT ( 'NONE',  ( -4.197312189423712425, -0.8182410726374559351, -3.202520316362482244 ) ) ;
#7520=DIRECTION ( 'NONE',  ( 0.000000000000000000, 0.000000000000000000, 1.000000000000000000 ) ) ;
#7529=AXIS2_PLACEMENT_3D ( 'NONE', #719, #15960, #11764 ) ;
#7530=CARTESIAN_POINT ( 'NONE',  ( -0.6937372685066658384, 4.453844082567720797, -3.310536846335889738 ) ) ;
#7550=ORIENTED_EDGE ( 'NONE', *, *, #11369, .F. ) ;
#7553=CARTESIAN_POINT ( 'NONE',  ( -2.000000000000002220, 3.464101615137751278, 0.000000000000000000 ) ) ;
#7556=ORIENTED_EDGE ( 'NONE', *, *, #11018, .T. ) ;
#7582=DIRECTION ( 'NONE',  ( 0.000000000000000000, 0.000000000000000000, -1.000000000000000000 ) ) ;
#7591=DIRECTION ( 'NONE',  ( 0.000000000000000000, 0.000000000000000000, 1.000000000000000000 ) ) ;
#7633=CARTESIAN_POINT ( 'NONE',  ( 3.999999999999998224, -2.309401076758513582, -0.5000000000000000000 ) ) ;
#7639=ORIENTED_EDGE ( 'NONE', *, *, #1321, .F. ) ;
#7644=CARTESIAN_POINT ( 'NONE',  ( 3.455075492488604016, -2.624013387858240787, -3.016622336522134518 ) ) ;
#7649=CARTESIAN_POINT ( 'NONE',  ( -1.655952806101419927, 3.662737355149035423, -2.077348303141170793E-15 ) ) ;
#7656=CARTESIAN_POINT ( 'NONE',  ( 2.344047193898586734, 3.265465875126468465, -1.231162388834125148E-15 ) ) ;
#7680=CARTESIAN_POINT ( 'NONE',  ( 2.500000000000000888, 0.000000000000000000, -4.699999999999999289 ) ) ;
#7699=SURFACE_STYLE_USAGE ( .BOTH. , #3527 ) ;
#7707=DIRECTION ( 'NONE',  ( -0.000000000000000000, -0.000000000000000000, 1.000000000000000000 ) ) ;
#7716=VERTEX_POINT ( 'NONE', #10724 ) ;
#7765=EDGE_LOOP ( 'NONE', ( #776, #11827, #13808, #6151, #16615 ) ) ;
#7787=FILL_AREA_STYLE_COLOUR ( '', #5432 ) ;
#7793=DIRECTION ( 'NONE',  ( 0.000000000000000000, 0.000000000000000000, 1.000000000000000000 ) ) ;
#7816=CARTESIAN_POINT ( 'NONE',  ( -0.1404055950190654656, -4.699865361597007407, -3.386887224136973185 ) ) ;
#7819=ORIENTED_EDGE ( 'NONE', *, *, #9237, .F. ) ;
#7832=DIRECTION ( 'NONE',  ( -0.000000000000000000, -0.000000000000000000, 1.000000000000000000 ) ) ;
#7845=FACE_OUTER_BOUND ( 'NONE', #2971, .T. ) ;
#7927=ORIENTED_EDGE ( 'NONE', *, *, #14584, .F. ) ;
#7947=DIRECTION ( 'NONE',  ( 1.000000000000000000, 0.000000000000000000, 0.000000000000000000 ) ) ;
#7970=CARTESIAN_POINT ( 'NONE',  ( 4.197393957002304887, 7.725818140447171444E-14, -3.203767560748932208 ) ) ;
#7997=CARTESIAN_POINT ( 'NONE',  ( -1.390214784104961021, -4.043996922316171805, -3.202509183706246265 ) ) ;
#8001=CARTESIAN_POINT ( 'NONE',  ( -4.000000000000000000, -2.309401076758508253, -3.133295621305383083 ) ) ;
#8009=CARTESIAN_POINT ( 'NONE',  ( 4.000000000000004441, -2.309401076758508697, -3.204271511726787924 ) ) ;
#8055=CARTESIAN_POINT ( 'NONE',  ( 1.393927851585477828, -4.043713361053538513, -3.226374918436841099 ) ) ;
#8065=AXIS2_PLACEMENT_3D ( 'NONE', #3134, #8848, #7582 ) ;
#8085=AXIS2_PLACEMENT_3D ( 'NONE', #15192, #11257, #1509 ) ;
#8097=CARTESIAN_POINT ( 'NONE',  ( -2.038300084272748336E-14, -4.618802153517010289, -0.5000000000000000000 ) ) ;
#8101=DIRECTION ( 'NONE',  ( 0.000000000000000000, 0.000000000000000000, -1.000000000000000000 ) ) ;
#8124=AXIS2_PLACEMENT_3D ( 'NONE', #6180, #830, #3289 ) ;
#8131=AXIS2_PLACEMENT_3D ( 'NONE', #11509, #17817, #2466 ) ;
#8143=CARTESIAN_POINT ( 'NONE',  ( -3.199999999999999289, 4.408728476930471151E-16, 2.399999999999999467 ) ) ;
#8157=CONICAL_SURFACE ( 'NONE', #3223, 3.999999999999998224, 0.8911886515913775009 ) ;
#8168=FACE_OUTER_BOUND ( 'NONE', #13558, .T. ) ;
#8180=CARTESIAN_POINT ( 'NONE',  ( -3.472352378023116692, -2.614038573344128924, -3.020318136128631981 ) ) ;
#8182=CONICAL_SURFACE ( 'NONE', #950, 3.999999999999998224, 0.8911886515913775009 ) ;
#8189=VECTOR ( 'NONE', #13205, 1000.000000000000000 ) ;
#8204=CARTESIAN_POINT ( 'NONE',  ( -4.207491450040567571, 2.029819825146473189, -3.371670828759567140 ) ) ;
#8221=VERTEX_POINT ( 'NONE', #8492 ) ;
#8229=CARTESIAN_POINT ( 'NONE',  ( 0.000000000000000000, 0.000000000000000000, 0.000000000000000000 ) ) ;
#8236=CARTESIAN_POINT ( 'NONE',  ( 0.6937372685066659495, -4.453844082567731455, -3.310536846335892847 ) ) ;
#8258=CARTESIAN_POINT ( 'NONE',  ( 4.000000000000000000, 2.309401076758498483, -3.133295621305380863 ) ) ;
#8260=DIRECTION ( 'NONE',  ( 0.8191520442889900222, 1.003171929053522528E-16, -0.5735764363510486019 ) ) ;
#8291=UNCERTAINTY_MEASURE_WITH_UNIT (LENGTH_MEASURE( 1.000000000000000082E-05 ), #9216, 'distance_accuracy_value', 'NONE');
#8326=EDGE_CURVE ( 'NONE', #12636, #13340, #11656, .T. ) ;
#8335=B_SPLINE_CURVE_WITH_KNOTS ( 'NONE', 3,
 ( #13124, #4947, #6135, #787, #9041 ),
 .UNSPECIFIED., .F., .F.,
 ( 4, 1, 4 ),
 ( 0.000000000000000000, 0.002309401076758505356, 0.004618802153517009845 ),
 .UNSPECIFIED. ) ;
#8344=B_SPLINE_CURVE_WITH_KNOTS ( 'NONE', 3,
 ( #697, #16033, #8856, #17312, #2246, #1975 ),
 .UNSPECIFIED., .F., .F.,
 ( 4, 2, 4 ),
 ( 0.002365888236227995951, 0.003551327329835086283, 0.004736766423442176181 ),
 .UNSPECIFIED. ) ;
#8362=CARTESIAN_POINT ( 'NONE',  ( 4.000000000000000000, 1.680235903636325023, -3.016633206402969503 ) ) ;
#8390=ORIENTED_EDGE ( 'NONE', *, *, #17406, .F. ) ;
#8402=PLANE ( 'NONE',  #9619 ) ;
#8414=DIRECTION ( 'NONE',  ( 1.000000000000000000, 0.000000000000000000, 0.000000000000000000 ) ) ;
#8420=( BOUNDED_SURFACE ( )  B_SPLINE_SURFACE ( 3, 2, ( 
 ( #13214, #15846, #13483 ),
 ( #12019, #6318, #4950 ),
 ( #6138, #10478, #2254 ),
 ( #13300, #5041, #10564 ),
 ( #12372, #15272, #10993 ),
 ( #1144, #2773, #13821 ) ),
 .UNSPECIFIED., .F., .F., .T. ) 
 B_SPLINE_SURFACE_WITH_KNOTS ( ( 4, 2, 4 ),
 ( 3, 3 ),
 ( 0.02023740217035200836, 0.02269762987400599646, 0.02515785757765998457 ),
 ( 0.000000000000000000, 1.000000000000000000 ),
 .UNSPECIFIED. ) 
 GEOMETRIC_REPRESENTATION_ITEM ( )  RATIONAL_B_SPLINE_SURFACE ( (
 ( 1.000000000000000000, 0.8047781539129729156, 1.000000000000000000),
 ( 1.000000000000000000, 0.8123770319056426992, 1.000000000000000000),
 ( 1.000000000000000000, 0.8190663783057815506, 1.000000000000000000),
 ( 1.000000000000000000, 0.8192359702876089722, 1.000000000000000000),
 ( 1.000000000000000000, 0.8126134888420550872, 1.000000000000000000),
 ( 1.000000000000000000, 0.8047712368238109093, 1.000000000000000000) ) ) 
 REPRESENTATION_ITEM ( '' )  SURFACE ( )  );
#8434=B_SPLINE_CURVE_WITH_KNOTS ( 'NONE', 3,
 ( #7221, #12731, #10092, #5834, #8661, #16735, #7313, #12832 ),
 .UNSPECIFIED., .F., .F.,
 ( 4, 2, 2, 4 ),
 ( 0.005725059856848623528, 0.006314084072593609265, 0.006903108288338595869, 0.008081156719828567342 ),
 .UNSPECIFIED. ) ;
#8438=B_SPLINE_CURVE_WITH_KNOTS ( 'NONE', 3,
 ( #15099, #16646, #3951, #12294, #5563, #16389 ),
 .UNSPECIFIED., .F., .F.,
 ( 4, 2, 4 ),
 ( 0.003358874760055536278, 0.004541967308452079903, 0.005725059856848623528 ),
 .UNSPECIFIED. ) ;
#8447=CARTESIAN_POINT ( 'NONE',  ( 0.000000000000000000, 0.000000000000000000, -4.674599999999997202 ) ) ;
#8472=AXIS2_PLACEMENT_3D ( 'NONE', #418, #9815, #15364 ) ;
#8484=EDGE_CURVE ( 'NONE', #7158, #14985, #2739, .T. ) ;
#8486=LINE ( 'NONE', #12379, #2287 ) ;
#8492=CARTESIAN_POINT ( 'NONE',  ( 3.000000000000000000, 0.000000000000000000, 2.399999999999999467 ) ) ;
#8507=EDGE_CURVE ( 'NONE', #7462, #12543, #8344, .T. ) ;
#8511=ORIENTED_EDGE ( 'NONE', *, *, #1321, .T. ) ;
#8513=VERTEX_POINT ( 'NONE', #7680 ) ;
#8517=CARTESIAN_POINT ( 'NONE',  ( 2.100000000000000089, 0.000000000000000000, 1.159999999999999476 ) ) ;
#8578=ADVANCED_FACE ( 'NONE', ( #4507, #4420 ), #1623, .F. ) ;
#8588=EDGE_CURVE ( 'NONE', #5981, #16863, #4230, .T. ) ;
#8600=B_SPLINE_CURVE_WITH_KNOTS ( 'NONE', 3,
 ( #9281, #8009, #13548, #17754, #9536, #14821 ),
 .UNSPECIFIED., .F., .F.,
 ( 4, 2, 4 ),
 ( 0.000000000000000000, 0.0002095117440854733380, 0.0004190234881709466760 ),
 .UNSPECIFIED. ) ;
#8609=CARTESIAN_POINT ( 'NONE',  ( 4.000000000000000000, -2.309401076758510918, -4.700000000000000178 ) ) ;
#8618=DIRECTION ( 'NONE',  ( -0.9396926207859143121, 0.000000000000000000, -0.3420201433256525592 ) ) ;
#8647=ORIENTED_EDGE ( 'NONE', *, *, #15646, .T. ) ;
#8661=CARTESIAN_POINT ( 'NONE',  ( -4.000000000000000000, 0.9868501483902580862, -0.09357334158579672101 ) ) ;
#8675=EDGE_CURVE ( 'NONE', #11660, #4375, #8335, .T. ) ;
#8682=CARTESIAN_POINT ( 'NONE',  ( -4.204114099329565590, 1.660341531092949685, -3.302132361967891061 ) ) ;
#8698=ORIENTED_EDGE ( 'NONE', *, *, #6148, .F. ) ;
#8710=CARTESIAN_POINT ( 'NONE',  ( 0.000000000000000000, 0.000000000000000000, 1.599999999999999423 ) ) ;
#8715=PLANE ( 'NONE',  #17769 ) ;
#8716=DIRECTION ( 'NONE',  ( 0.000000000000000000, 0.000000000000000000, 1.000000000000000000 ) ) ;
#8723=ADVANCED_FACE ( 'NONE', ( #464 ), #5869, .T. ) ;
#8738=CONICAL_SURFACE ( 'NONE', #10453, 3.999999999999998224, 0.8911886515913775009 ) ;
#8747=CARTESIAN_POINT ( 'NONE',  ( -4.154094228333307548, 2.398367420968273489, -3.421909803043222897 ) ) ;
#8755=DIRECTION ( 'NONE',  ( -0.000000000000000000, -0.000000000000000000, 1.000000000000000000 ) ) ;
#8776=CARTESIAN_POINT ( 'NONE',  ( -4.000000000000000000, -0.8382426107201325083, -2.920612530944983298 ) ) ;
#8783=DIRECTION ( 'NONE',  ( -0.000000000000000000, -0.000000000000000000, 1.000000000000000000 ) ) ;
#8791=VERTEX_POINT ( 'NONE', #1645 ) ;
#8797=DIRECTION ( 'NONE',  ( -1.000000000000000000, 0.000000000000000000, 0.000000000000000000 ) ) ;
#8804=PRODUCT_DEFINITION_CONTEXT ( 'detailed design', #2061, 'design' ) ;
#8838=EDGE_CURVE ( 'NONE', #13298, #2020, #17207, .T. ) ;
#8848=DIRECTION ( 'NONE',  ( 0.000000000000000000, -1.000000000000000000, 0.000000000000000000 ) ) ;
#8856=CARTESIAN_POINT ( 'NONE',  ( -2.682243648011669368, -3.070208061305314207, -0.04852650426602043987 ) ) ;
#8863=CARTESIAN_POINT ( 'NONE',  ( -3.586207239825857747E-13, 4.796734841935103688, -3.421909803043224230 ) ) ;
#8888=DIRECTION ( 'NONE',  ( -0.000000000000000000, -0.000000000000000000, 1.000000000000000000 ) ) ;
#8919=CARTESIAN_POINT ( 'NONE',  ( -4.000000000000004441, 2.309401076758499816, -3.204269196027524913 ) ) ;
#8973=CARTESIAN_POINT ( 'NONE',  ( 1.243649364574536075E-15, 4.862606272033089816, -3.445885042887437244 ) ) ;
#8988=DIRECTION ( 'NONE',  ( -1.000000000000000000, 0.000000000000000000, 0.000000000000000000 ) ) ;
#8995=CARTESIAN_POINT ( 'NONE',  ( 0.5469803261931410754, -4.303002914948000246, -3.235259548910958127 ) ) ;
#9022=CARTESIAN_POINT ( 'NONE',  ( -1.391697335622809950, -4.043246145443384343, -3.203898532754370532 ) ) ;
#9038=TOROIDAL_SURFACE ( 'NONE', #16551, 5.384454397937117776, 0.5155456020628805813 ) ;
#9041=CARTESIAN_POINT ( 'NONE',  ( -4.000000000000000000, 2.309401076758501592, -3.133295621305381307 ) ) ;
#9052=AXIS2_PLACEMENT_3D ( 'NONE', #10924, #17801, #5321 ) ;
#9054=ORIENTED_EDGE ( 'NONE', *, *, #9088, .T. ) ;
#9056=CARTESIAN_POINT ( 'NONE',  ( 4.000000000000000000, 2.309401076758498483, -4.700000000000000178 ) ) ;
#9065=CIRCLE ( 'NONE', #3569, 3.999999999999999112 ) ;
#9072=EDGE_LOOP ( 'NONE', ( #14852, #8698, #2355, #9269 ) ) ;
#9088=EDGE_CURVE ( 'NONE', #11785, #8791, #12542, .T. ) ;
#9089=CARTESIAN_POINT ( 'NONE',  ( -4.000000000000000000, -2.309401076758508253, -3.133295621305383083 ) ) ;
#9098=EDGE_LOOP ( 'NONE', ( #5617, #5467, #1380, #2604 ) ) ;
#9117=DIRECTION ( 'NONE',  ( 1.000000000000000000, 0.000000000000000000, 0.000000000000000000 ) ) ;
#9121=ORIENTED_EDGE ( 'NONE', *, *, #2301, .T. ) ;
#9142=EDGE_CURVE ( 'NONE', #3354, #7716, #9790, .T. ) ;
#9149=ORIENTED_EDGE ( 'NONE', *, *, #11753, .T. ) ;
#9162=ORIENTED_EDGE ( 'NONE', *, *, #3910, .F. ) ;
#9163=CARTESIAN_POINT ( 'NONE',  ( 5.560781378645575757, 0.000000000000000000, -3.700000000000000178 ) ) ;
#9181=EDGE_CURVE ( 'NONE', #364, #2020, #13268, .T. ) ;
#9191=EDGE_CURVE ( 'NONE', #5051, #4413, #16760, .T. ) ;
#9205=VERTEX_POINT ( 'NONE', #17137 ) ;
#9216=( LENGTH_UNIT ( ) NAMED_UNIT ( * ) SI_UNIT ( .MILLI., .METRE. ) );
#9237=EDGE_CURVE ( 'NONE', #7716, #16729, #4332, .T. ) ;
#9245=AXIS2_PLACEMENT_3D ( 'NONE', #258, #8783, #11569 ) ;
#9248=ORIENTED_EDGE ( 'NONE', *, *, #16533, .F. ) ;
#9254=CARTESIAN_POINT ( 'NONE',  ( 1.257202807339943496, -3.892955774273574310, -3.133250573521610516 ) ) ;
#9259=CARTESIAN_POINT ( 'NONE',  ( 0.000000000000000000, 0.000000000000000000, 1.599999999999998979 ) ) ;
#9260=DIRECTION ( 'NONE',  ( 1.000000000000000000, 0.000000000000000000, 0.000000000000000000 ) ) ;
#9261=CARTESIAN_POINT ( 'NONE',  ( 0.6448876103708347518, 4.246476118072353145, -0.2256878752776725616 ) ) ;
#9269=ORIENTED_EDGE ( 'NONE', *, *, #13314, .F. ) ;
#9272=DIRECTION ( 'NONE',  ( 1.000000000000000000, 0.000000000000000000, 0.000000000000000000 ) ) ;
#9281=CARTESIAN_POINT ( 'NONE',  ( 4.000000000000000000, -2.309401076758510918, -3.133295621305383083 ) ) ;
#9342=CARTESIAN_POINT ( 'NONE',  ( 1.360615521534834782, -4.061278559077730499, -3.205052026701941781 ) ) ;
#9351=DIRECTION ( 'NONE',  ( -0.000000000000000000, -0.000000000000000000, 1.000000000000000000 ) ) ;
#9358=CARTESIAN_POINT ( 'NONE',  ( 3.679171394226031122, 2.494631558665831861, -0.3503314178412501589 ) ) ;
#9361=LINE ( 'NONE', #1037, #15111 ) ;
#9370=EDGE_LOOP ( 'NONE', ( #6819, #2799, #10895, #12668, #7491 ) ) ;
#9385=( NAMED_UNIT ( * ) PLANE_ANGLE_UNIT ( ) SI_UNIT ( $, .RADIAN. ) );
#9433=CARTESIAN_POINT ( 'NONE',  ( -0.1756478951291671753, 4.720212513052427283, -3.169390900447852655 ) ) ;
#9434=CARTESIAN_POINT ( 'NONE',  ( -3.453019673806803524, -2.625200315327865130, -3.235259548910208505 ) ) ;
#9453=DIRECTION ( 'NONE',  ( 1.000000000000000000, 0.000000000000000000, 0.000000000000000000 ) ) ;
#9477=VERTEX_POINT ( 'NONE', #53 ) ;
#9506=FACE_OUTER_BOUND ( 'NONE', #944, .T. ) ;
#9509=CARTESIAN_POINT ( 'NONE',  ( 0.000000000000000000, 0.000000000000000000, 0.000000000000000000 ) ) ;
#9519=CARTESIAN_POINT ( 'NONE',  ( -4.235887314095728939, -2.417314327725974543, -3.451162025751987272 ) ) ;
#9536=CARTESIAN_POINT ( 'NONE',  ( 4.154306624731438191, -2.398490048084426896, -3.421999068284419465 ) ) ;
#9537=FACE_OUTER_BOUND ( 'NONE', #6637, .T. ) ;
#9541=ADVANCED_FACE ( 'NONE', ( #10730 ), #13887, .T. ) ;
#9550=CARTESIAN_POINT ( 'NONE',  ( 0.000000000000000000, 0.000000000000000000, 0.000000000000000000 ) ) ;
#9557=DIRECTION ( 'NONE',  ( -0.000000000000000000, -0.000000000000000000, 1.000000000000000000 ) ) ;
#9563=VERTEX_POINT ( 'NONE', #12295 ) ;
#9581=DIRECTION ( 'NONE',  ( -0.000000000000000000, -0.000000000000000000, 1.000000000000000000 ) ) ;
#9594=CARTESIAN_POINT ( 'NONE',  ( 0.000000000000000000, 0.000000000000000000, -4.184454397937119374 ) ) ;
#9601=CARTESIAN_POINT ( 'NONE',  ( 2.500000000000000888, 3.061616997868384127E-16, -4.674599999999997202 ) ) ;
#9603=CARTESIAN_POINT ( 'NONE',  ( -0.6810530063608482010, -4.461079733298037198, -3.298443181296194293 ) ) ;
#9608=B_SPLINE_CURVE_WITH_KNOTS ( 'NONE', 3,
 ( #12078, #17664, #6911, #12174, #14902, #5186 ),
 .UNSPECIFIED., .F., .F.,
 ( 4, 2, 4 ),
 ( 0.000000000000000000, 0.0002095117440854733651, 0.0004190234881709467302 ),
 .UNSPECIFIED. ) ;
#9619=AXIS2_PLACEMENT_3D ( 'NONE', #1429, #9840, #11013 ) ;
#9642=DIRECTION ( 'NONE',  ( -0.000000000000000000, -0.000000000000000000, 1.000000000000000000 ) ) ;
#9647=DIRECTION ( 'NONE',  ( 0.000000000000000000, 0.000000000000000000, -1.000000000000000000 ) ) ;
#9658=DIRECTION ( 'NONE',  ( 0.000000000000000000, 0.000000000000000000, 1.000000000000000000 ) ) ;
#9704=DIRECTION ( 'NONE',  ( 1.000000000000000000, 0.000000000000000000, 0.000000000000000000 ) ) ;
#9728=DIRECTION ( 'NONE',  ( -1.000000000000000000, 0.000000000000000000, 0.000000000000000000 ) ) ;
#9739=EDGE_CURVE ( 'NONE', #364, #2889, #8434, .T. ) ;
#9763=CARTESIAN_POINT ( 'NONE',  ( -2.000000000000002220, 3.464101615137751278, 0.000000000000000000 ) ) ;
#9781=ORIENTED_EDGE ( 'NONE', *, *, #10733, .F. ) ;
#9790=CIRCLE ( 'NONE', #9245, 2.100000000000000089 ) ;
#9796=CARTESIAN_POINT ( 'NONE',  ( 4.197478771013683385, -0.8523759490158154817, -3.205061274276559846 ) ) ;
#9815=DIRECTION ( 'NONE',  ( -0.000000000000000000, -0.000000000000000000, 1.000000000000000000 ) ) ;
#9827=B_SPLINE_CURVE_WITH_KNOTS ( 'NONE', 3,
 ( #7448, #5700, #12968, #553, #469, #11217 ),
 .UNSPECIFIED., .F., .F.,
 ( 4, 2, 4 ),
 ( 0.002452478801916362864, 0.003676905084147999610, 0.004901331366379636789 ),
 .UNSPECIFIED. ) ;
#9838=EDGE_CURVE ( 'NONE', #14231, #7158, #2620, .T. ) ;
#9840=DIRECTION ( 'NONE',  ( -1.000000000000000000, 0.000000000000000000, 0.000000000000000000 ) ) ;
#9844=CARTESIAN_POINT ( 'NONE',  ( -2.100000000000000089, 2.571758278209441957E-16, -4.700000000000000178 ) ) ;
#9848=VECTOR ( 'NONE', #4450, 1000.000000000000000 ) ;
#9863=CARTESIAN_POINT ( 'NONE',  ( 2.000000000000002665, -3.464101615137751278, 0.000000000000000000 ) ) ;
#9875=AXIS2_PLACEMENT_3D ( 'NONE', #2556, #10779, #9260 ) ;
#9908=ORIENTED_EDGE ( 'NONE', *, *, #13392, .T. ) ;
#9922=ORIENTED_EDGE ( 'NONE', *, *, #16533, .T. ) ;
#9927=ORIENTED_EDGE ( 'NONE', *, *, #5868, .F. ) ;
#9939=VERTEX_POINT ( 'NONE', #4834 ) ;
#9953=CARTESIAN_POINT ( 'NONE',  ( -2.345747346278106438, 3.264484291692491436, -0.01223254789873562572 ) ) ;
#9958=ORIENTED_EDGE ( 'NONE', *, *, #3636, .F. ) ;
#9997=EDGE_CURVE ( 'NONE', #16703, #364, #17128, .T. ) ;
#10015=EDGE_LOOP ( 'NONE', ( #12656, #10397, #3442, #6567, #2551, #9922, #6925 ) ) ;
#10017=CARTESIAN_POINT ( 'NONE',  ( -4.000000000000000000, 1.677751148815738391, -3.235249634003040775 ) ) ;
#10019=CARTESIAN_POINT ( 'NONE',  ( 8.409399735147211686E-16, 4.618802153517009401, -3.133295621305383083 ) ) ;
#10083=ORIENTED_EDGE ( 'NONE', *, *, #14298, .T. ) ;
#10088=ORIENTED_EDGE ( 'NONE', *, *, #8326, .F. ) ;
#10089=DIRECTION ( 'NONE',  ( -1.000000000000000000, 0.000000000000000000, 0.000000000000000000 ) ) ;
#10092=CARTESIAN_POINT ( 'NONE',  ( -4.000000000000000000, 0.3987449864459981508, -0.01220643443059921812 ) ) ;
#10123=EDGE_CURVE ( 'NONE', #5056, #5499, #283, .T. ) ;
#10124=ORIENTED_EDGE ( 'NONE', *, *, #1378, .F. ) ;
#10133=FACE_OUTER_BOUND ( 'NONE', #4117, .T. ) ;
#10147=DIRECTION ( 'NONE',  ( 1.000000000000000000, 0.000000000000000000, 0.000000000000000000 ) ) ;
#10152=EDGE_CURVE ( 'NONE', #5499, #10872, #3792, .T. ) ;
#10256=FACE_OUTER_BOUND ( 'NONE', #17404, .T. ) ;
#10271=CARTESIAN_POINT ( 'NONE',  ( -4.000000000000000000, -2.309401076758508253, -4.700000000000000178 ) ) ;
#10275=CARTESIAN_POINT ( 'NONE',  ( -2.449848172108561428, -3.432307619358749395, -3.203702292528910700 ) ) ;
#10308=DIRECTION ( 'NONE',  ( 0.000000000000000000, 0.000000000000000000, 1.000000000000000000 ) ) ;
#10327=CARTESIAN_POINT ( 'NONE',  ( 4.000000000000000888, 0.9868501483902626381, -0.09357334158579776184 ) ) ;
#10350=ORIENTED_EDGE ( 'NONE', *, *, #14140, .T. ) ;
#10351=DIRECTION ( 'NONE',  ( -0.000000000000000000, -0.000000000000000000, 1.000000000000000000 ) ) ;
#10392=AXIS2_PLACEMENT_3D ( 'NONE', #7013, #15174, #1665 ) ;
#10397=ORIENTED_EDGE ( 'NONE', *, *, #8326, .T. ) ;
#10399=ADVANCED_FACE ( 'NONE', ( #16475 ), #2642, .T. ) ;
#10419=CARTESIAN_POINT ( 'NONE',  ( 2.687328764639639544, -3.067272167851296416, -0.05923475698271170320 ) ) ;
#10421=ORIENTED_EDGE ( 'NONE', *, *, #14584, .T. ) ;
#10430=CARTESIAN_POINT ( 'NONE',  ( -0.02448804030507887100, -4.877043185438137307, -3.451162025751992157 ) ) ;
#10445=CARTESIAN_POINT ( 'NONE',  ( -1.312671235360379107, -3.860931062424225235, -0.05923475698271177259 ) ) ;
#10447=LINE ( 'NONE', #6555, #16904 ) ;
#10453=AXIS2_PLACEMENT_3D ( 'NONE', #4675, #514, #1698 ) ;
#10462=AXIS2_PLACEMENT_3D ( 'NONE', #11037, #12054, #10679 ) ;
#10468=VERTEX_POINT ( 'NONE', #2536 ) ;
#10472=CARTESIAN_POINT ( 'NONE',  ( 4.000000000000000000, -0.7890432684750885439, -0.04868663549882413372 ) ) ;
#10478=CARTESIAN_POINT ( 'NONE',  ( -1.257202807338834605, 3.892955774274010849, -3.133250573521422222 ) ) ;
#10482=APPLICATION_CONTEXT ( 'automotive_design' ) ;
#10515=CARTESIAN_POINT ( 'NONE',  ( 4.000000000000000000, 0.7924765000094643463, -0.05906175389889926214 ) ) ;
#10528=CARTESIAN_POINT ( 'NONE',  ( 2.836862643238821313, 3.208966885971292538, -3.205052026701870282 ) ) ;
#10550=ORIENTED_EDGE ( 'NONE', *, *, #13991, .T. ) ;
#10554=CARTESIAN_POINT ( 'NONE',  ( -4.000000000000000000, 2.309401076758501592, -4.700000000000000178 ) ) ;
#10555=CARTESIAN_POINT ( 'NONE',  ( -4.211140560182196957, -2.431303136016548017, -3.445885042887436356 ) ) ;
#10557=ORIENTED_EDGE ( 'NONE', *, *, #1518, .T. ) ;
#10564=CARTESIAN_POINT ( 'NONE',  ( -2.807096675500661664, 3.225959780909132490, -3.202509183706299112 ) ) ;
#10575=VERTEX_POINT ( 'NONE', #10672 ) ;
#10607=CARTESIAN_POINT ( 'NONE',  ( 3.035766082959412415E-15, 4.618802153517010289, -0.5000000000000000000 ) ) ;
#10627=CARTESIAN_POINT ( 'NONE',  ( 0.000000000000000000, 0.000000000000000000, -3.700000000000000178 ) ) ;
#10629=VECTOR ( 'NONE', #7520, 1000.000000000000000 ) ;
#10643=CIRCLE ( 'NONE', #2840, 5.560781378645573980 ) ;
#10645=( NAMED_UNIT ( * ) SI_UNIT ( $, .STERADIAN. ) SOLID_ANGLE_UNIT ( ) );
#10653=ORIENTED_EDGE ( 'NONE', *, *, #9191, .F. ) ;
#10672=CARTESIAN_POINT ( 'NONE',  ( 2.000000000000002665, -3.464101615137751278, 0.000000000000000000 ) ) ;
#10679=DIRECTION ( 'NONE',  ( 1.000000000000000000, 0.000000000000000000, 0.000000000000000000 ) ) ;
#10681=CARTESIAN_POINT ( 'NONE',  ( 2.807096675499403116, -3.225959780909533503, -3.202509183706199636 ) ) ;
#10687=CARTESIAN_POINT ( 'NONE',  ( 4.140405595019059248, 2.228337868678515132, -3.386887224136966079 ) ) ;
#10698=CARTESIAN_POINT ( 'NONE',  ( 4.000000000000000000, 2.309401076758510918, -0.5000000000000000000 ) ) ;
#10723=AXIS2_PLACEMENT_3D ( 'NONE', #6796, #4073, #15136 ) ;
#10724=CARTESIAN_POINT ( 'NONE',  ( -2.100000000000000089, 2.571758278209441957E-16, -4.394516984716110741 ) ) ;
#10728=CONICAL_SURFACE ( 'NONE', #15990, 2.500000000000000888, 0.9599310885968781459 ) ;
#10730=FACE_OUTER_BOUND ( 'NONE', #6310, .T. ) ;
#10731=SHAPE_REPRESENTATION_RELATIONSHIP ( 'NONE' , 'NONE' ,  #1480, #7249 ) ;
#10733=EDGE_CURVE ( 'NONE', #8513, #5051, #4082, .T. ) ;
#10741=CIRCLE ( 'NONE', #4396, 3.999999999999998224 ) ;
#10764=ORIENTED_EDGE ( 'NONE', *, *, #8507, .F. ) ;
#10776=VECTOR ( 'NONE', #17837, 1000.000000000000000 ) ;
#10779=DIRECTION ( 'NONE',  ( 0.000000000000000000, 0.000000000000000000, 1.000000000000000000 ) ) ;
#10797=FACE_BOUND ( 'NONE', #1171, .T. ) ;
#10813=ORIENTED_EDGE ( 'NONE', *, *, #7293, .T. ) ;
#10830=EDGE_LOOP ( 'NONE', ( #4460, #10083, #7287, #7556, #10550, #339 ) ) ;
#10831=ORIENTED_EDGE ( 'NONE', *, *, #2225, .F. ) ;
#10872=VERTEX_POINT ( 'NONE', #7385 ) ;
#10873=CARTESIAN_POINT ( 'NONE',  ( -7.511572993685817836E-16, -4.618802153517020059, -3.133295621305386636 ) ) ;
#10886=EDGE_CURVE ( 'NONE', #16703, #14159, #5469, .T. ) ;
#10895=ORIENTED_EDGE ( 'NONE', *, *, #968, .T. ) ;
#10896=FACE_OUTER_BOUND ( 'NONE', #6128, .T. ) ;
#10898=VECTOR ( 'NONE', #8260, 1000.000000000000000 ) ;
#10924=CARTESIAN_POINT ( 'NONE',  ( 8.409399735147211686E-16, 4.618802153517009401, -4.700000000000000178 ) ) ;
#10939=CIRCLE ( 'NONE', #6339, 2.500000000000000888 ) ;
#10951=ORIENTED_EDGE ( 'NONE', *, *, #11698, .T. ) ;
#10961=CARTESIAN_POINT ( 'NONE',  ( 0.000000000000000000, 0.000000000000000000, 1.599999999999998979 ) ) ;
#10990=AXIS2_PLACEMENT_3D ( 'NONE', #16975, #6168, #4531 ) ;
#10992=UNCERTAINTY_MEASURE_WITH_UNIT (LENGTH_MEASURE( 1.000000000000000082E-05 ), #13485, 'distance_accuracy_value', 'NONE');
#10993=CARTESIAN_POINT ( 'NONE',  ( -3.522881874162667515, 2.820349071481667025, -3.298443181295974469 ) ) ;
#10995=SURFACE_SIDE_STYLE ('',( #4774 ) ) ;
#11013=DIRECTION ( 'NONE',  ( 0.000000000000000000, 0.000000000000000000, 1.000000000000000000 ) ) ;
#11018=EDGE_CURVE ( 'NONE', #10575, #3955, #635, .T. ) ;
#11037=CARTESIAN_POINT ( 'NONE',  ( 0.000000000000000000, 0.000000000000000000, 13.31572692736085095 ) ) ;
#11051=CARTESIAN_POINT ( 'NONE',  ( -0.5636734750060078403, -4.293365120987107986, -3.231543764078805836 ) ) ;
#11054=CIRCLE ( 'NONE', #3269, 3.199999999999999289 ) ;
#11081=ORIENTED_EDGE ( 'NONE', *, *, #15574, .F. ) ;
#11145=DIRECTION ( 'NONE',  ( 0.000000000000000000, 0.000000000000000000, 1.000000000000000000 ) ) ;
#11192=ORIENTED_EDGE ( 'NONE', *, *, #8507, .T. ) ;
#11202=CARTESIAN_POINT ( 'NONE',  ( -2.500000000000000888, 3.061616997868384127E-16, -4.699999999999999289 ) ) ;
#11217=CARTESIAN_POINT ( 'NONE',  ( 4.211140560182196957, -2.431303136016550237, -3.445885042887436800 ) ) ;
#11222=VERTEX_POINT ( 'NONE', #5754 ) ;
#11236=CARTESIAN_POINT ( 'NONE',  ( 4.000000000000000000, -1.700153365595038268, -3.020323189000620800 ) ) ;
#11237=ORIENTED_EDGE ( 'NONE', *, *, #7326, .F. ) ;
#11239=AXIS2_PLACEMENT_3D ( 'NONE', #9259, #17824, #2737 ) ;
#11248=AXIS2_PLACEMENT_3D ( 'NONE', #7256, #8797, #10308 ) ;
#11253=EDGE_CURVE ( 'NONE', #6928, #13340, #11304, .T. ) ;
#11257=DIRECTION ( 'NONE',  ( 0.000000000000000000, 0.000000000000000000, -1.000000000000000000 ) ) ;
#11265=ORIENTED_EDGE ( 'NONE', *, *, #603, .T. ) ;
#11275=CARTESIAN_POINT ( 'NONE',  ( 0.000000000000000000, 0.000000000000000000, -3.700000000000000178 ) ) ;
#11304=CIRCLE ( 'NONE', #2941, 0.5155456020628804703 ) ;
#11313=CARTESIAN_POINT ( 'NONE',  ( 2.100000000000000089, 0.000000000000000000, -4.700000000000000178 ) ) ;
#11314=ORIENTED_EDGE ( 'NONE', *, *, #15032, .F. ) ;
#11321=ADVANCED_FACE ( 'NONE', ( #15655 ), #8738, .T. ) ;
#11325=VECTOR ( 'NONE', #3002, 1000.000000000000000 ) ;
#11332=CARTESIAN_POINT ( 'NONE',  ( -0.3208286057739646036, 4.433571671609678688, -0.3503314178412559321 ) ) ;
#11369=EDGE_CURVE ( 'NONE', #4375, #2889, #5112, .T. ) ;
#11398=ORIENTED_EDGE ( 'NONE', *, *, #13608, .T. ) ;
#11401=PLANE ( 'NONE',  #11248 ) ;
#11437=CARTESIAN_POINT ( 'NONE',  ( -4.024497503033519941, 2.323544716729378568, -3.272167766733379946 ) ) ;
#11440=ORIENTED_EDGE ( 'NONE', *, *, #1989, .F. ) ;
#11451=SHAPE_DEFINITION_REPRESENTATION ( #12298, #1480 ) ;
#11469=CARTESIAN_POINT ( 'NONE',  ( 3.861362476283256129, 2.629030857715989988, -3.371615880910371565 ) ) ;
#11470=CARTESIAN_POINT ( 'NONE',  ( 3.999999999999999112, -1.539600717839008981, -3.000726591567081769 ) ) ;
#11473=DIRECTION ( 'NONE',  ( -0.000000000000000000, -0.000000000000000000, 1.000000000000000000 ) ) ;
#11487=DIRECTION ( 'NONE',  ( -1.000000000000000000, 0.000000000000000000, -0.000000000000000000 ) ) ;
#11509=CARTESIAN_POINT ( 'NONE',  ( 0.000000000000000000, 0.000000000000000000, -4.700000000000000178 ) ) ;
#11521=ORIENTED_EDGE ( 'NONE', *, *, #3345, .F. ) ;
#11522=CONICAL_SURFACE ( 'NONE', #1393, 3.999999999999998224, 0.8911886515913775009 ) ;
#11524=( BOUNDED_SURFACE ( )  B_SPLINE_SURFACE ( 3, 2, ( 
 ( #12427, #12, #9519 ),
 ( #8180, #9434, #16519 ),
 ( #13621, #4189, #6549 ),
 ( #4095, #16266, #7997 ),
 ( #1108, #11051, #9603 ),
 ( #16613, #12065, #1374 ) ),
 .UNSPECIFIED., .F., .F., .T. ) 
 B_SPLINE_SURFACE_WITH_KNOTS ( ( 4, 2, 4 ),
 ( 3, 3 ),
 ( 0.02023740217035201530, 0.02269762987400599993, 0.02515785757765998457 ),
 ( 0.000000000000000000, 1.000000000000000000 ),
 .UNSPECIFIED. ) 
 GEOMETRIC_REPRESENTATION_ITEM ( )  RATIONAL_B_SPLINE_SURFACE ( (
 ( 1.000000000000000000, 0.8047781539129733597, 1.000000000000000000),
 ( 1.000000000000000000, 0.8123770319057486144, 1.000000000000000000),
 ( 1.000000000000000000, 0.8190663783056398861, 1.000000000000000000),
 ( 1.000000000000000000, 0.8192359702877524130, 1.000000000000000000),
 ( 1.000000000000000000, 0.8126134888419467295, 1.000000000000000000),
 ( 1.000000000000000000, 0.8047712368238109093, 1.000000000000000000) ) ) 
 REPRESENTATION_ITEM ( '' )  SURFACE ( )  );
#11554=ORIENTED_EDGE ( 'NONE', *, *, #2049, .F. ) ;
#11562=DIRECTION ( 'NONE',  ( 1.000000000000000000, 0.000000000000000000, 0.000000000000000000 ) ) ;
#11563=B_SPLINE_CURVE_WITH_KNOTS ( 'NONE', 3,
 ( #783, #611, #517, #10472, #4764, #4587 ),
 .UNSPECIFIED., .F., .F.,
 ( 4, 2, 4 ),
 ( 0.003358874760055540181, 0.004541967308452085107, 0.005725059856848630467 ),
 .UNSPECIFIED. ) ;
#11569=DIRECTION ( 'NONE',  ( -1.000000000000000000, 0.000000000000000000, 0.000000000000000000 ) ) ;
#11593=EDGE_LOOP ( 'NONE', ( #14802, #8511, #16661, #12325, #7550 ) ) ;
#11656=LINE ( 'NONE', #6496, #8189 ) ;
#11660=VERTEX_POINT ( 'NONE', #15813 ) ;
#11661=CARTESIAN_POINT ( 'NONE',  ( 2.804994570502172380, 3.229033611042450680, -3.226374918436836214 ) ) ;
#11667=FILL_AREA_STYLE_COLOUR ( '', #5354 ) ;
#11684=CARTESIAN_POINT ( 'NONE',  ( -3.511755186886750479, 2.826662030176367413, -3.297382984111579596 ) ) ;
#11698=EDGE_CURVE ( 'NONE', #4061, #16943, #16511, .T. ) ;
#11751=( NAMED_UNIT ( * ) PLANE_ANGLE_UNIT ( ) SI_UNIT ( $, .RADIAN. ) );
#11753=EDGE_CURVE ( 'NONE', #14985, #9477, #6962, .T. ) ;
#11757=ORIENTED_EDGE ( 'NONE', *, *, #9997, .T. ) ;
#11764=DIRECTION ( 'NONE',  ( 1.000000000000000000, 0.000000000000000000, 0.000000000000000000 ) ) ;
#11773=DIRECTION ( 'NONE',  ( 1.000000000000000000, 0.000000000000000000, 0.000000000000000000 ) ) ;
#11780=CARTESIAN_POINT ( 'NONE',  ( 3.333333333333333925, -2.694301256218262886, -3.000726591567083545 ) ) ;
#11783=CARTESIAN_POINT ( 'NONE',  ( -4.000000000000000000, 2.309401076758501592, -3.133295621305381307 ) ) ;
#11785=VERTEX_POINT ( 'NONE', #12166 ) ;
#11786=EDGE_CURVE ( 'NONE', #8221, #10468, #6666, .T. ) ;
#11787=CYLINDRICAL_SURFACE ( 'NONE', #8131, 2.100000000000000089 ) ;
#11816=CARTESIAN_POINT ( 'NONE',  ( -5.816800114226745675E-16, -4.862606272033100474, -3.445885042887441241 ) ) ;
#11827=ORIENTED_EDGE ( 'NONE', *, *, #1689, .F. ) ;
#11831=ORIENTED_EDGE ( 'NONE', *, *, #1543, .F. ) ;
#11865=LINE ( 'NONE', #13422, #6724 ) ;
#11870=ORIENTED_EDGE ( 'NONE', *, *, #11018, .F. ) ;
#11876=ORIENTED_EDGE ( 'NONE', *, *, #13004, .T. ) ;
#11891=CARTESIAN_POINT ( 'NONE',  ( 1.390214784104990997, 4.043996922316214437, -3.202509183706264917 ) ) ;
#11908=DIRECTION ( 'NONE',  ( -0.000000000000000000, -0.000000000000000000, 1.000000000000000000 ) ) ;
#11957=CARTESIAN_POINT ( 'NONE',  ( -5.210193653659516369E-16, -4.647091401871165317, -3.272172305156515026 ) ) ;
#11966=CARTESIAN_POINT ( 'NONE',  ( 2.000000000000002665, -3.464101615137751278, 0.000000000000000000 ) ) ;
#11976=CARTESIAN_POINT ( 'NONE',  ( -4.000000000000000000, -2.168404344971008868E-15, -2.842992957459234304 ) ) ;
#11984=DIRECTION ( 'NONE',  ( 1.000000000000000000, 0.000000000000000000, 0.000000000000000000 ) ) ;
#11998=ORIENTED_EDGE ( 'NONE', *, *, #9088, .F. ) ;
#12000=CARTESIAN_POINT ( 'NONE',  ( -3.861362476283255241, -2.629030857715999314, -3.371615880910374230 ) ) ;
#12008=ORIENTED_EDGE ( 'NONE', *, *, #8838, .T. ) ;
#12011=CARTESIAN_POINT ( 'NONE',  ( -4.024497503033519941, -2.323544716729384785, -3.272167766733382166 ) ) ;
#12019=CARTESIAN_POINT ( 'NONE',  ( -0.5276476219778145627, 4.314164656930851827, -3.020318136128644859 ) ) ;
#12026=ORIENTED_EDGE ( 'NONE', *, *, #7422, .F. ) ;
#12054=DIRECTION ( 'NONE',  ( -0.000000000000000000, -0.000000000000000000, 1.000000000000000000 ) ) ;
#12064=CARTESIAN_POINT ( 'NONE',  ( 4.175003227304314279, 2.208362916365298911, -3.169254239516210880 ) ) ;
#12065=CARTESIAN_POINT ( 'NONE',  ( 0.1410420225375878522, -4.700232803196147557, -3.387027626239170530 ) ) ;
#12078=CARTESIAN_POINT ( 'NONE',  ( 4.000000000000000000, 2.309401076758498483, -3.133295621305380863 ) ) ;
#12101=ADVANCED_FACE ( 'NONE', ( #14537 ), #11787, .F. ) ;
#12166=CARTESIAN_POINT ( 'NONE',  ( -5.384454397937117776, 6.702023979852544604E-16, -4.700000000000000178 ) ) ;
#12174=CARTESIAN_POINT ( 'NONE',  ( 4.101954839143060916, 2.368264730582929634, -3.381130640444268032 ) ) ;
#12226=PLANE ( 'NONE',  #9052 ) ;
#12276=DIRECTION ( 'NONE',  ( -0.000000000000000000, -0.000000000000000000, 1.000000000000000000 ) ) ;
#12294=CARTESIAN_POINT ( 'NONE',  ( -4.000000000000000000, -0.7890432684750876557, -0.04868663549882429331 ) ) ;
#12295=CARTESIAN_POINT ( 'NONE',  ( 4.211140560182196957, 2.431303136016537803, -3.445885042887434579 ) ) ;
#12298=PRODUCT_DEFINITION_SHAPE ( 'NONE', 'NONE',  #15223 ) ;
#12325=ORIENTED_EDGE ( 'NONE', *, *, #9739, .T. ) ;
#12329=DIRECTION ( 'NONE',  ( 0.5000000000000014433, 0.8660254037844378194, -0.000000000000000000 ) ) ;
#12355=CARTESIAN_POINT ( 'NONE',  ( 4.211405962802042602, 2.460462805100870565, -3.451298870276226172 ) ) ;
#12372=CARTESIAN_POINT ( 'NONE',  ( -3.455075492487832634, 2.624013387858676438, -3.016622336521400882 ) ) ;
#12379=CARTESIAN_POINT ( 'NONE',  ( -7.511572993685817836E-16, -4.618802153517020059, -4.700000000000000178 ) ) ;
#12400=CIRCLE ( 'NONE', #15883, 2.100000000000000089 ) ;
#12427=CARTESIAN_POINT ( 'NONE',  ( -4.175003227304314279, -2.208362916365308681, -3.169254239516212657 ) ) ;
#12445=ADVANCED_FACE ( 'NONE', ( #2186 ), #540, .T. ) ;
#12471=CARTESIAN_POINT ( 'NONE',  ( -4.000000000000000000, -2.309401076758508253, -3.133295621305383083 ) ) ;
#12487=CARTESIAN_POINT ( 'NONE',  ( 0.000000000000000000, 0.000000000000000000, 1.599999999999998979 ) ) ;
#12538=CARTESIAN_POINT ( 'NONE',  ( -5.816800114226745675E-16, -4.862606272033100474, -3.445885042887441241 ) ) ;
#12539=FACE_OUTER_BOUND ( 'NONE', #17241, .T. ) ;
#12542=CIRCLE ( 'NONE', #100, 0.5155456020628804703 ) ;
#12543=VERTEX_POINT ( 'NONE', #17797 ) ;
#12590=DIRECTION ( 'NONE',  ( -0.000000000000000000, -0.000000000000000000, 1.000000000000000000 ) ) ;
#12627=CARTESIAN_POINT ( 'NONE',  ( 4.000000000000000000, 2.512222795755930438, -3.169391084040452000 ) ) ;
#12636=VERTEX_POINT ( 'NONE', #7970 ) ;
#12645=CARTESIAN_POINT ( 'NONE',  ( -4.197393957002304887, -7.639915766855272736E-14, -3.203767560748932208 ) ) ;
#12656=ORIENTED_EDGE ( 'NONE', *, *, #5702, .T. ) ;
#12661=CARTESIAN_POINT ( 'NONE',  ( 0.6920835326022570788, 4.454600218803882683, -3.297382984111581816 ) ) ;
#12662=CARTESIAN_POINT ( 'NONE',  ( 4.000000000000000888, 1.539600717838997435, -3.000726591567082213 ) ) ;
#12668=ORIENTED_EDGE ( 'NONE', *, *, #10886, .T. ) ;
#12672=ORIENTED_EDGE ( 'NONE', *, *, #4516, .T. ) ;
#12705=ORIENTED_EDGE ( 'NONE', *, *, #13235, .T. ) ;
#12713=EDGE_CURVE ( 'NONE', #3955, #4061, #4686, .T. ) ;
#12725=AXIS2_PLACEMENT_3D ( 'NONE', #11275, #13023, #16852 ) ;
#12731=CARTESIAN_POINT ( 'NONE',  ( -4.000000000000000000, 0.1981133338132469168, -1.407451120981426406E-15 ) ) ;
#12765=DIRECTION ( 'NONE',  ( -0.000000000000000000, -0.000000000000000000, 1.000000000000000000 ) ) ;
#12777=AXIS2_PLACEMENT_3D ( 'NONE', #1999, #13227, #12956 ) ;
#12788=LINE ( 'NONE', #4360, #12975 ) ;
#12812=CARTESIAN_POINT ( 'NONE',  ( -2.500000000000000888, 0.000000000000000000, -4.674599999999997202 ) ) ;
#12821=TOROIDAL_SURFACE ( 'NONE', #7344, 5.384454397937117776, 0.5155456020628805813 ) ;
#12832=CARTESIAN_POINT ( 'NONE',  ( -4.000000000000000000, 2.309401076758501592, -0.4999999999999963363 ) ) ;
#12837=CARTESIAN_POINT ( 'NONE',  ( -4.203833317240879275, -1.627343821129590307, -3.297273115243891439 ) ) ;
#12855=CARTESIAN_POINT ( 'NONE',  ( 4.000000000000000000, 2.309401076758498483, -3.133295621305380863 ) ) ;
#12866=ORIENTED_EDGE ( 'NONE', *, *, #14708, .T. ) ;
#12867=EDGE_LOOP ( 'NONE', ( #6756, #7443, #14643, #3020 ) ) ;
#12872=DIRECTION ( 'NONE',  ( 0.000000000000000000, 0.000000000000000000, -1.000000000000000000 ) ) ;
#12873=ADVANCED_FACE ( 'NONE', ( #15909 ), #4826, .T. ) ;
#12899=CARTESIAN_POINT ( 'NONE',  ( -1.317756351988338626, 3.857995168970202116, -0.04852650426601485406 ) ) ;
#12940=CARTESIAN_POINT ( 'NONE',  ( -5.384454397937117776, 6.594054843588580568E-16, -4.184454397937119374 ) ) ;
#12956=DIRECTION ( 'NONE',  ( 0.8660254037844380415, 0.5000000000000008882, 0.000000000000000000 ) ) ;
#12964=ORIENTED_EDGE ( 'NONE', *, *, #3490, .F. ) ;
#12967=FACE_OUTER_BOUND ( 'NONE', #17101, .T. ) ;
#12968=CARTESIAN_POINT ( 'NONE',  ( 4.198928548860774157, -0.8158838809860105012, -3.226471437616921012 ) ) ;
#12970=CARTESIAN_POINT ( 'NONE',  ( -7.511572993685817836E-16, -4.618802153517020059, -3.133295621305386636 ) ) ;
#12975=VECTOR ( 'NONE', #8618, 1000.000000000000000 ) ;
#13004=EDGE_CURVE ( 'NONE', #7158, #11222, #14090, .T. ) ;
#13023=DIRECTION ( 'NONE',  ( -0.000000000000000000, -0.000000000000000000, 1.000000000000000000 ) ) ;
#13062=CARTESIAN_POINT ( 'NONE',  ( 2.171643655288375996, -3.365003104552331870, -9.156896733678572738E-15 ) ) ;
#13073=VECTOR ( 'NONE', #9658, 1000.000000000000000 ) ;
#13075=CARTESIAN_POINT ( 'NONE',  ( -4.000000000000000000, 2.309401076758501592, -3.133295621305381307 ) ) ;
#13096=DIRECTION ( 'NONE',  ( 1.000000000000000000, 0.000000000000000000, 0.000000000000000000 ) ) ;
#13102=AXIS2_PLACEMENT_3D ( 'NONE', #5087, #9351, #11984 ) ;
#13111=ADVANCED_FACE ( 'NONE', ( #13533 ), #11524, .F. ) ;
#13124=CARTESIAN_POINT ( 'NONE',  ( 8.409399735147211686E-16, 4.618802153517009401, -3.133295621305383083 ) ) ;
#13146=CARTESIAN_POINT ( 'NONE',  ( -1.747541505913278614, 3.837784562140256650, -3.203702292528908924 ) ) ;
#13159=CARTESIAN_POINT ( 'NONE',  ( 4.000000000000000000, 0.3987449864459997606, -0.01220643443059902904 ) ) ;
#13168=CARTESIAN_POINT ( 'NONE',  ( -0.1750032273043209963, -4.719840313910222740, -3.169254239516217986 ) ) ;
#13183=EDGE_LOOP ( 'NONE', ( #9927, #223, #1657, #13477 ) ) ;
#13205=DIRECTION ( 'NONE',  ( 0.9396926207859143121, 1.150791560227857665E-16, -0.3420201433256525592 ) ) ;
#13214=CARTESIAN_POINT ( 'NONE',  ( 0.1750032273043211906, 4.719840313910212082, -3.169254239516213989 ) ) ;
#13221=ORIENTED_EDGE ( 'NONE', *, *, #13991, .F. ) ;
#13225=PRESENTATION_STYLE_ASSIGNMENT (( #7699 ) ) ;
#13227=DIRECTION ( 'NONE',  ( 0.5000000000000009992, -0.8660254037844381525, 0.000000000000000000 ) ) ;
#13235=EDGE_CURVE ( 'NONE', #11222, #8791, #12788, .T. ) ;
#13253=ORIENTED_EDGE ( 'NONE', *, *, #6148, .T. ) ;
#13266=CARTESIAN_POINT ( 'NONE',  ( -0.3198814748697748067, -4.434118497892180599, -0.3507732604232522977 ) ) ;
#13268=LINE ( 'NONE', #14644, #10776 ) ;
#13285=ADVANCED_FACE ( 'NONE', ( #14429 ), #11522, .T. ) ;
#13292=ORIENTED_EDGE ( 'NONE', *, *, #2534, .F. ) ;
#13298=VERTEX_POINT ( 'NONE', #14620 ) ;
#13300=CARTESIAN_POINT ( 'NONE',  ( -2.725758460534118743, 3.045084772581732491, -2.920601398289153661 ) ) ;
#13314=EDGE_CURVE ( 'NONE', #9477, #5981, #4999, .T. ) ;
#13337=EDGE_CURVE ( 'NONE', #2327, #10575, #7168, .T. ) ;
#13340=VERTEX_POINT ( 'NONE', #9163 ) ;
#13346=CARTESIAN_POINT ( 'NONE',  ( 0.5276476219768818643, -4.314164656931400721, -3.020318136128620434 ) ) ;
#13366=CARTESIAN_POINT ( 'NONE',  ( 0.000000000000000000, 0.000000000000000000, 0.000000000000000000 ) ) ;
#13388=AXIS2_PLACEMENT_3D ( 'NONE', #13750, #1062, #5303 ) ;
#13390=CARTESIAN_POINT ( 'NONE',  ( -2.000000000000005329, -3.464101615137750390, 0.000000000000000000 ) ) ;
#13392=EDGE_CURVE ( 'NONE', #5056, #16729, #12400, .T. ) ;
#13409=ORIENTED_EDGE ( 'NONE', *, *, #2917, .T. ) ;
#13422=CARTESIAN_POINT ( 'NONE',  ( 3.000000000000000000, 0.000000000000000000, 13.31572692736085095 ) ) ;
#13472=CARTESIAN_POINT ( 'NONE',  ( 2.500000000000000888, 3.061616997868384127E-16, -4.674599999999997202 ) ) ;
#13477=ORIENTED_EDGE ( 'NONE', *, *, #2848, .F. ) ;
#13483=CARTESIAN_POINT ( 'NONE',  ( 0.02448804030507906182, 4.877043185438126649, -3.451162025751988160 ) ) ;
#13485=( LENGTH_UNIT ( ) NAMED_UNIT ( * ) SI_UNIT ( .MILLI., .METRE. ) );
#13525=DIRECTION ( 'NONE',  ( -0.000000000000000000, -0.000000000000000000, 1.000000000000000000 ) ) ;
#13533=FACE_OUTER_BOUND ( 'NONE', #2439, .T. ) ;
#13540=CARTESIAN_POINT ( 'NONE',  ( -0.6666666666666676289, -4.233901974057269868, -3.000726591567087098 ) ) ;
#13548=CARTESIAN_POINT ( 'NONE',  ( 4.024499207728656103, -2.323545700935583547, -3.272172305156509697 ) ) ;
#13558=EDGE_LOOP ( 'NONE', ( #13292, #10124, #16633, #4050 ) ) ;
#13565=DIRECTION ( 'NONE',  ( -1.000000000000000000, 0.000000000000000000, 0.000000000000000000 ) ) ;
#13571=FACE_OUTER_BOUND ( 'NONE', #2571, .T. ) ;
#13579=EDGE_CURVE ( 'NONE', #3428, #4413, #10939, .T. ) ;
#13603=EDGE_LOOP ( 'NONE', ( #5301, #12026 ) ) ;
#13608=EDGE_CURVE ( 'NONE', #11785, #6928, #7492, .T. ) ;
#13621=CARTESIAN_POINT ( 'NONE',  ( -2.756166666307358071, -3.027528586792987753, -2.923144239647250231 ) ) ;
#13655=( NAMED_UNIT ( * ) SI_UNIT ( $, .STERADIAN. ) SOLID_ANGLE_UNIT ( ) );
#13684=EDGE_CURVE ( 'NONE', #6928, #11785, #2003, .T. ) ;
#13700=CYLINDRICAL_SURFACE ( 'NONE', #15098, 3.000000000000000000 ) ;
#13717=CARTESIAN_POINT ( 'NONE',  ( -2.000000000000000444, -3.464101615137763268, -2.842992957459239189 ) ) ;
#13731=CARTESIAN_POINT ( 'NONE',  ( -4.211140560182196957, 2.431303136016540911, -3.445885042887435468 ) ) ;
#13750=CARTESIAN_POINT ( 'NONE',  ( 0.000000000000000000, 0.000000000000000000, 1.599999999999998979 ) ) ;
#13756=ORIENTED_EDGE ( 'NONE', *, *, #4516, .F. ) ;
#13796=ORIENTED_EDGE ( 'NONE', *, *, #8675, .F. ) ;
#13808=ORIENTED_EDGE ( 'NONE', *, *, #4753, .F. ) ;
#13818=ADVANCED_FACE ( 'NONE', ( #2856 ), #1723, .T. ) ;
#13821=CARTESIAN_POINT ( 'NONE',  ( -4.236525418537980592, 2.416953631397924074, -3.451298686683625050 ) ) ;
#13824=EDGE_CURVE ( 'NONE', #16729, #5056, #4892, .T. ) ;
#13854=AXIS2_PLACEMENT_3D ( 'NONE', #16303, #1409, #13565 ) ;
#13868=CYLINDRICAL_SURFACE ( 'NONE', #10462, 4.000000000000000000 ) ;
#13887=CONICAL_SURFACE ( 'NONE', #15627, 5.560781378645573980, 1.221730476396047926 ) ;
#13893=CARTESIAN_POINT ( 'NONE',  ( 4.204114824917600579, -1.660420935435634737, -3.302147294767050489 ) ) ;
#13910=CARTESIAN_POINT ( 'NONE',  ( 0.000000000000000000, 0.000000000000000000, 1.599999999999998979 ) ) ;
#13929=B_SPLINE_CURVE_WITH_KNOTS ( 'NONE', 3,
 ( #3580, #13266, #5010, #17383, #10445, #581, #6377, #2138 ),
 .UNSPECIFIED., .F., .F.,
 ( 4, 2, 2, 4 ),
 ( 2.465131517309074801E-07, 0.001183067374689863224, 0.001774477805458929370, 0.002365888236227995951 ),
 .UNSPECIFIED. ) ;
#13933=CARTESIAN_POINT ( 'NONE',  ( -4.211140560182196957, -2.431303136016548017, -3.445885042887436356 ) ) ;
#13937=CARTESIAN_POINT ( 'NONE',  ( 0.000000000000000000, 2.540000000000001368, 1.599999999999999423 ) ) ;
#13950=ORIENTED_EDGE ( 'NONE', *, *, #5702, .F. ) ;
#13991=EDGE_CURVE ( 'NONE', #3955, #13298, #683, .T. ) ;
#14033=CARTESIAN_POINT ( 'NONE',  ( 1.764121045782362237E-15, 4.736522675502163437, -3.381124513963625233 ) ) ;
#14038=DIRECTION ( 'NONE',  ( 0.000000000000000000, 0.000000000000000000, 1.000000000000000000 ) ) ;
#14084=EDGE_LOOP ( 'NONE', ( #7819, #3324, #16827, #9908 ) ) ;
#14090=B_SPLINE_CURVE_WITH_KNOTS ( 'NONE', 3,
 ( #7317, #12837, #4490, #12645 ),
 .UNSPECIFIED., .F., .F.,
 ( 4, 4 ),
 ( 0.000000000000000000, 0.002452478801916373706 ),
 .UNSPECIFIED. ) ;
#14096=CYLINDRICAL_SURFACE ( 'NONE', #8472, 3.000000000000000000 ) ;
#14140=EDGE_CURVE ( 'NONE', #5981, #9205, #8600, .T. ) ;
#14152=AXIS2_PLACEMENT_3D ( 'NONE', #86, #12765, #15402 ) ;
#14159=VERTEX_POINT ( 'NONE', #6562 ) ;
#14160=ADVANCED_FACE ( 'NONE', ( #10797, #16372 ), #17844, .F. ) ;
#14177=CARTESIAN_POINT ( 'NONE',  ( 0.000000000000000000, 0.000000000000000000, 1.599999999999998979 ) ) ;
#14203=VECTOR ( 'NONE', #7591, 1000.000000000000000 ) ;
#14209=CARTESIAN_POINT ( 'NONE',  ( -4.000000000000000000, -2.512220432843121909, -3.169390650195385906 ) ) ;
#14211=CARTESIAN_POINT ( 'NONE',  ( 1.391697335622810838, 4.043246145443373685, -3.203898532754367867 ) ) ;
#14231=VERTEX_POINT ( 'NONE', #12538 ) ;
#14248=CARTESIAN_POINT ( 'NONE',  ( 2.540000000000001368, 0.000000000000000000, 1.599999999999998979 ) ) ;
#14284=EDGE_LOOP ( 'NONE', ( #6476, #17096, #15266, #10831 ) ) ;
#14298=EDGE_CURVE ( 'NONE', #364, #7462, #5764, .T. ) ;
#14301=ORIENTED_EDGE ( 'NONE', *, *, #17524, .T. ) ;
#14313=ORIENTED_EDGE ( 'NONE', *, *, #7293, .F. ) ;
#14337=EDGE_LOOP ( 'NONE', ( #11831, #7927, #17199 ) ) ;
#14340=DIRECTION ( 'NONE',  ( -0.000000000000000000, -0.000000000000000000, 1.000000000000000000 ) ) ;
#14343=CARTESIAN_POINT ( 'NONE',  ( 2.345747346278109990, -3.264484291692499873, -0.01223254789874230961 ) ) ;
#14362=EDGE_LOOP ( 'NONE', ( #5151, #11081, #8647, #5737 ) ) ;
#14394=CARTESIAN_POINT ( 'NONE',  ( 1.750546785592199463E-15, 4.647089433458765129, -3.272167766733383054 ) ) ;
#14419=CARTESIAN_POINT ( 'NONE',  ( -7.511572993685816850E-16, -4.618802153517020059, -3.204271511726792365 ) ) ;
#14424=ORIENTED_EDGE ( 'NONE', *, *, #13824, .F. ) ;
#14429=FACE_OUTER_BOUND ( 'NONE', #14337, .T. ) ;
#14450=AXIS2_PLACEMENT_3D ( 'NONE', #15492, #12590, #8414 ) ;
#14497=AXIS2_PLACEMENT_3D ( 'NONE', #17314, #971, #7947 ) ;
#14510=CYLINDRICAL_SURFACE ( 'NONE', #7529, 2.100000000000000089 ) ;
#14521=ORIENTED_EDGE ( 'NONE', *, *, #13684, .T. ) ;
#14537=FACE_OUTER_BOUND ( 'NONE', #13183, .T. ) ;
#14548=CARTESIAN_POINT ( 'NONE',  ( 3.540000644887451031, 2.810673041921355697, -3.302142222889115519 ) ) ;
#14584=EDGE_CURVE ( 'NONE', #14159, #4061, #2537, .T. ) ;
#14620=CARTESIAN_POINT ( 'NONE',  ( 3.999999999999999112, 0.000000000000000000, 1.599999999999998979 ) ) ;
#14636=CARTESIAN_POINT ( 'NONE',  ( 2.742797192660275662, 3.035247456002220900, -3.133250573521050519 ) ) ;
#14643=ORIENTED_EDGE ( 'NONE', *, *, #3636, .T. ) ;
#14644=CARTESIAN_POINT ( 'NONE',  ( -4.000000000000000000, 4.898587196589412829E-16, 13.31572692736085095 ) ) ;
#14650=CARTESIAN_POINT ( 'NONE',  ( -3.510273485745307731, -2.827716139362665082, -3.310536846335889738 ) ) ;
#14673=FACE_OUTER_BOUND ( 'NONE', #872, .T. ) ;
#14693=LINE ( 'NONE', #2275, #6098 ) ;
#14708=EDGE_CURVE ( 'NONE', #3354, #3428, #4357, .T. ) ;
#14772=VECTOR ( 'NONE', #14038, 1000.000000000000000 ) ;
#14802=ORIENTED_EDGE ( 'NONE', *, *, #1689, .T. ) ;
#14806=CARTESIAN_POINT ( 'NONE',  ( 1.144235203016664926, 3.958177651039091582, -0.09382832055445673725 ) ) ;
#14812=CARTESIAN_POINT ( 'NONE',  ( 3.349226789952651995, 2.685125164760732819, -0.2236248678334793738 ) ) ;
#14821=CARTESIAN_POINT ( 'NONE',  ( 4.211140560182196957, -2.431303136016550237, -3.445885042887436800 ) ) ;
#14823=ORIENTED_EDGE ( 'NONE', *, *, #13608, .F. ) ;
#14852=ORIENTED_EDGE ( 'NONE', *, *, #1084, .T. ) ;
#14858=CARTESIAN_POINT ( 'NONE',  ( 3.000000000000000000, 0.000000000000000000, 1.599999999999998979 ) ) ;
#14875=B_SPLINE_CURVE_WITH_KNOTS ( 'NONE', 3,
 ( #4681, #8863, #14033, #14394, #4506, #10019 ),
 .UNSPECIFIED., .F., .F.,
 ( 4, 2, 4 ),
 ( -3.640115492407988208E-06, 0.0002066546034006553050, 0.0004169493222937186317 ),
 .UNSPECIFIED. ) ;
#14889=CARTESIAN_POINT ( 'NONE',  ( 1.287221018261662353, 3.875624752116917371, -3.130620751972434501 ) ) ;
#14902=CARTESIAN_POINT ( 'NONE',  ( 4.154306624730766728, 2.398490048085576642, -3.421999068284416357 ) ) ;
#14907=ADVANCED_FACE ( 'NONE', ( #12967 ), #8715, .T. ) ;
#14942=ADVANCED_FACE ( 'NONE', ( #13571 ), #17944, .F. ) ;
#14985=VERTEX_POINT ( 'NONE', #12471 ) ;
#14988=CARTESIAN_POINT ( 'NONE',  ( 3.999999999999998224, 0.000000000000000000, 0.000000000000000000 ) ) ;
#14995=CARTESIAN_POINT ( 'NONE',  ( -4.198928548860774157, 0.8158838809860086139, -3.226471437616920124 ) ) ;
#14996=ORIENTED_EDGE ( 'NONE', *, *, #15533, .T. ) ;
#15032=EDGE_CURVE ( 'NONE', #10872, #5499, #16564, .T. ) ;
#15033=CARTESIAN_POINT ( 'NONE',  ( -3.199999999999998845, 3.918869757271528981E-16, 1.599999999999999423 ) ) ;
#15041=CARTESIAN_POINT ( 'NONE',  ( 0.000000000000000000, 0.000000000000000000, -4.674599999999997202 ) ) ;
#15045=PRODUCT ( 'torque nut 04-2_iso_ISO 7043-M5-N', 'torque nut 04-2_iso_ISO 7043-M5-N', '', ( #15642 ) ) ;
#15053=DIRECTION ( 'NONE',  ( 0.000000000000000000, 0.000000000000000000, -1.000000000000000000 ) ) ;
#15083=CARTESIAN_POINT ( 'NONE',  ( 4.211399264691416455, -2.459727859270661288, -3.451161839612817861 ) ) ;
#15098=AXIS2_PLACEMENT_3D ( 'NONE', #1283, #6805, #2731 ) ;
#15099=CARTESIAN_POINT ( 'NONE',  ( -4.000000000000000000, -2.309401076758510918, -0.5000000000000000000 ) ) ;
#15111=VECTOR ( 'NONE', #2483, 1000.000000000000000 ) ;
#15130=AXIS2_PLACEMENT_3D ( 'NONE', #6585, #9557, #5478 ) ;
#15136=DIRECTION ( 'NONE',  ( 1.000000000000000000, 0.000000000000000000, 0.000000000000000000 ) ) ;
#15150=DIRECTION ( 'NONE',  ( 1.000000000000000000, 0.000000000000000000, 0.000000000000000000 ) ) ;
#15164=DIRECTION ( 'NONE',  ( 0.000000000000000000, 0.000000000000000000, -1.000000000000000000 ) ) ;
#15166=CARTESIAN_POINT ( 'NONE',  ( 0.000000000000000000, 0.000000000000000000, 2.399999999999999467 ) ) ;
#15174=DIRECTION ( 'NONE',  ( 0.000000000000000000, 0.000000000000000000, 1.000000000000000000 ) ) ;
#15192=CARTESIAN_POINT ( 'NONE',  ( 0.000000000000000000, 0.000000000000000000, -3.700000000000000178 ) ) ;
#15206=( GEOMETRIC_REPRESENTATION_CONTEXT ( 3 ) GLOBAL_UNCERTAINTY_ASSIGNED_CONTEXT ( ( #10992 ) ) GLOBAL_UNIT_ASSIGNED_CONTEXT ( ( #13485, #9385, #13655 ) ) REPRESENTATION_CONTEXT ( 'NONE', 'WORKASPACE' ) );
#15210=DIRECTION ( 'NONE',  ( 1.224646799147353207E-16, 1.000000000000000000, 0.000000000000000000 ) ) ;
#15212=CARTESIAN_POINT ( 'NONE',  ( 2.805705207896067144, -3.226868319750166858, -3.203898532754369644 ) ) ;
#15223=PRODUCT_DEFINITION ( 'UNKNOWN', '', #5985, #8804 ) ;
#15266=ORIENTED_EDGE ( 'NONE', *, *, #7422, .T. ) ;
#15272=CARTESIAN_POINT ( 'NONE',  ( -3.436326524993698062, 2.634838109288787145, -3.231543764077259517 ) ) ;
#15364=DIRECTION ( 'NONE',  ( 1.000000000000000000, 0.000000000000000000, 0.000000000000000000 ) ) ;
#15388=DIRECTION ( 'NONE',  ( 1.000000000000000000, 0.000000000000000000, 0.000000000000000000 ) ) ;
#15402=DIRECTION ( 'NONE',  ( 1.000000000000000000, 0.000000000000000000, 0.000000000000000000 ) ) ;
#15418=CARTESIAN_POINT ( 'NONE',  ( 1.655952806101423924, -3.662737355149043861, -9.025983085941824413E-15 ) ) ;
#15433=FACE_OUTER_BOUND ( 'NONE', #12867, .T. ) ;
#15459=ADVANCED_FACE ( 'NONE', ( #16023 ), #12821, .T. ) ;
#15471=ADVANCED_FACE ( 'NONE', ( #2877 ), #8402, .T. ) ;
#15489=ORIENTED_EDGE ( 'NONE', *, *, #13684, .F. ) ;
#15492=CARTESIAN_POINT ( 'NONE',  ( 0.000000000000000000, 0.000000000000000000, -4.700000000000000178 ) ) ;
#15506=CARTESIAN_POINT ( 'NONE',  ( -3.999999999999999112, 4.898587196589411843E-16, 1.599999999999998979 ) ) ;
#15533=EDGE_CURVE ( 'NONE', #7100, #4903, #11054, .T. ) ;
#15565=CARTESIAN_POINT ( 'NONE',  ( -4.000000000000000000, 2.511479357205540275, -3.169254599242374404 ) ) ;
#15574=EDGE_CURVE ( 'NONE', #131, #9563, #1033, .T. ) ;
#15627=AXIS2_PLACEMENT_3D ( 'NONE', #4222, #1243, #6932 ) ;
#15642=PRODUCT_CONTEXT ( 'NONE', #10482, 'mechanical' ) ;
#15646=EDGE_CURVE ( 'NONE', #131, #11660, #14875, .T. ) ;
#15655=FACE_OUTER_BOUND ( 'NONE', #6864, .T. ) ;
#15660=CARTESIAN_POINT ( 'NONE',  ( -4.000000000000000000, 0.8730390046629853407, -2.923132639555973800 ) ) ;
#15698=DIRECTION ( 'NONE',  ( -1.000000000000000000, 0.000000000000000000, 0.000000000000000000 ) ) ;
#15778=CARTESIAN_POINT ( 'NONE',  ( -8.661840944284252430E-17, -4.736529461165884136, -3.381130640444275581 ) ) ;
#15806=CARTESIAN_POINT ( 'NONE',  ( 0.000000000000000000, 0.000000000000000000, 0.000000000000000000 ) ) ;
#15808=DIRECTION ( 'NONE',  ( -0.8191520442889900222, 0.000000000000000000, -0.5735764363510486019 ) ) ;
#15811=EDGE_LOOP ( 'NONE', ( #12008, #9121, #14313, #11521 ) ) ;
#15813=CARTESIAN_POINT ( 'NONE',  ( 8.409399735147211686E-16, 4.618802153517009401, -3.133295621305383083 ) ) ;
#15846=CARTESIAN_POINT ( 'NONE',  ( 0.1404055950190656876, 4.699865361596996749, -3.386887224136968300 ) ) ;
#15882=CARTESIAN_POINT ( 'NONE',  ( 3.999999999999998224, 1.941961291383482280, -0.3515519931180262625 ) ) ;
#15883=AXIS2_PLACEMENT_3D ( 'NONE', #3454, #4713, #10147 ) ;
#15909=FACE_OUTER_BOUND ( 'NONE', #10830, .T. ) ;
#15923=AXIS2_PLACEMENT_3D ( 'NONE', #4204, #11145, #9704 ) ;
#15941=CARTESIAN_POINT ( 'NONE',  ( 4.197393957002304887, 0.8151795401431362054, -3.203767560748937537 ) ) ;
#15945=CIRCLE ( 'NONE', #1746, 3.199999999999999289 ) ;
#15948=EDGE_CURVE ( 'NONE', #2020, #13298, #9065, .T. ) ;
#15958=FILL_AREA_STYLE ('',( #7787 ) ) ;
#15960=DIRECTION ( 'NONE',  ( 0.000000000000000000, 0.000000000000000000, 1.000000000000000000 ) ) ;
#15969=CARTESIAN_POINT ( 'NONE',  ( 0.000000000000000000, 0.000000000000000000, 1.599999999999998979 ) ) ;
#15990=AXIS2_PLACEMENT_3D ( 'NONE', #8447, #15164, #197 ) ;
#16021=B_SPLINE_CURVE_WITH_KNOTS ( 'NONE', 3,
 ( #8258, #17903, #1103, #5083, #17648 ),
 .UNSPECIFIED., .F., .F.,
 ( 4, 1, 4 ),
 ( 0.000000000000000000, 0.002309401076758504923, 0.004618802153517009845 ),
 .UNSPECIFIED. ) ;
#16023=FACE_OUTER_BOUND ( 'NONE', #17927, .T. ) ;
#16033=CARTESIAN_POINT ( 'NONE',  ( -2.344047193898589398, -3.265465875126477346, -8.103564206381888188E-15 ) ) ;
#16039=AXIS2_PLACEMENT_3D ( 'NONE', #8710, #5970, #1922 ) ;
#16057=( LENGTH_UNIT ( ) NAMED_UNIT ( * ) SI_UNIT ( .MILLI., .METRE. ) );
#16064=ADVANCED_FACE ( 'NONE', ( #10896 ), #8182, .T. ) ;
#16096=MECHANICAL_DESIGN_GEOMETRIC_PRESENTATION_REPRESENTATION('',(#3928),#15206);
#16120=CARTESIAN_POINT ( 'NONE',  ( -4.000000000000000888, -2.309401076758508253, -3.204269196027527133 ) ) ;
#16122=CARTESIAN_POINT ( 'NONE',  ( 2.500000000000000888, 0.000000000000000000, -25.03750572909317285 ) ) ;
#16142=ORIENTED_EDGE ( 'NONE', *, *, #11253, .T. ) ;
#16166=ADVANCED_FACE ( 'NONE', ( #4303 ), #14096, .F. ) ;
#16234=CIRCLE ( 'NONE', #12725, 5.560781378645573980 ) ;
#16255=AXIS2_PLACEMENT_3D ( 'NONE', #1926, #14340, #7446 ) ;
#16256=CARTESIAN_POINT ( 'NONE',  ( 4.175647895129167786, -2.207990717223094812, -3.169390900447852655 ) ) ;
#16264=CARTESIAN_POINT ( 'NONE',  ( 1.312671235360370892, 3.860931062424219462, -0.05923475698270563861 ) ) ;
#16265=CARTESIAN_POINT ( 'NONE',  ( 3.453019673806209333, 2.625200315326833067, -3.235259548910759619 ) ) ;
#16266=CARTESIAN_POINT ( 'NONE',  ( -1.287221018261747618, -3.875624752117063920, -3.130620751971695093 ) ) ;
#16277=DIRECTION ( 'NONE',  ( 0.000000000000000000, 0.000000000000000000, 1.000000000000000000 ) ) ;
#16303=CARTESIAN_POINT ( 'NONE',  ( 0.000000000000000000, 0.000000000000000000, -4.394516984716110741 ) ) ;
#16333=CARTESIAN_POINT ( 'NONE',  ( 4.211140560182196957, -2.431303136016550237, -3.445885042887436800 ) ) ;
#16372=FACE_OUTER_BOUND ( 'NONE', #5531, .T. ) ;
#16373=DIRECTION ( 'NONE',  ( 1.000000000000000000, 0.000000000000000000, 0.000000000000000000 ) ) ;
#16389=CARTESIAN_POINT ( 'NONE',  ( -3.999999999999998224, 0.000000000000000000, 0.000000000000000000 ) ) ;
#16415=EDGE_CURVE ( 'NONE', #16863, #9563, #9608, .T. ) ;
#16453=CARTESIAN_POINT ( 'NONE',  ( 4.203935404774564510, 1.640788256319079208, -3.298453876328896861 ) ) ;
#16457=VECTOR ( 'NONE', #8716, 1000.000000000000000 ) ;
#16475=FACE_OUTER_BOUND ( 'NONE', #6166, .T. ) ;
#16479=VERTEX_POINT ( 'NONE', #8097 ) ;
#16482=ORIENTED_EDGE ( 'NONE', *, *, #4753, .T. ) ;
#16484=( NAMED_UNIT ( * ) PLANE_ANGLE_UNIT ( ) SI_UNIT ( $, .RADIAN. ) );
#16509=FACE_OUTER_BOUND ( 'NONE', #4391, .T. ) ;
#16511=B_SPLINE_CURVE_WITH_KNOTS ( 'NONE', 3,
 ( #2137, #7656, #759, #14812, #9358, #10698 ),
 .UNSPECIFIED., .F., .F.,
 ( 4, 2, 4 ),
 ( 0.002365888236227992047, 0.003551327329835083247, 0.004736766423442174447 ),
 .UNSPECIFIED. ) ;
#16515=CARTESIAN_POINT ( 'NONE',  ( 4.000000000000000000, -2.309401076758510918, -3.133295621305383083 ) ) ;
#16519=CARTESIAN_POINT ( 'NONE',  ( -3.540000644887186798, -2.810673041920830784, -3.302142222888937884 ) ) ;
#16523=DIRECTION ( 'NONE',  ( -0.000000000000000000, -0.000000000000000000, 1.000000000000000000 ) ) ;
#16533=EDGE_CURVE ( 'NONE', #6357, #131, #5723, .T. ) ;
#16535=DIRECTION ( 'NONE',  ( 1.000000000000000000, 0.000000000000000000, 0.000000000000000000 ) ) ;
#16551=AXIS2_PLACEMENT_3D ( 'NONE', #9594, #13525, #15150 ) ;
#16564=CIRCLE ( 'NONE', #13388, 2.540000000000001368 ) ;
#16579=FACE_OUTER_BOUND ( 'NONE', #9370, .T. ) ;
#16580=CARTESIAN_POINT ( 'NONE',  ( 3.511755186886750479, -2.826662030176377627, -3.297382984111582260 ) ) ;
#16604=FACE_OUTER_BOUND ( 'NONE', #7414, .T. ) ;
#16612=( BOUNDED_SURFACE ( )  B_SPLINE_SURFACE ( 3, 2, ( 
 ( #17845, #6830, #15083 ),
 ( #11236, #1486, #13893 ),
 ( #4288, #2666, #9796 ),
 ( #5630, #5364, #16814 ),
 ( #8362, #4378, #16453 ),
 ( #12627, #4114, #12355 ) ),
 .UNSPECIFIED., .F., .F., .T. ) 
 B_SPLINE_SURFACE_WITH_KNOTS ( ( 4, 2, 4 ),
 ( 3, 3 ),
 ( 0.02018219363417822834, 0.02264238182714342976, 0.02510257002010863117 ),
 ( 0.000000000000000000, 1.000000000000000000 ),
 .UNSPECIFIED. ) 
 GEOMETRIC_REPRESENTATION_ITEM ( )  RATIONAL_B_SPLINE_SURFACE ( (
 ( 1.000000000000000000, 0.8047781633350724606, 1.000000000000000000),
 ( 1.000000000000000000, 0.8123767859461582530, 1.000000000000000000),
 ( 1.000000000000000000, 0.8190657615682832571, 1.000000000000000000),
 ( 1.000000000000000000, 0.8192365618914938530, 1.000000000000000000),
 ( 1.000000000000000000, 0.8126137554627823611, 1.000000000000000000),
 ( 1.000000000000000000, 0.8047712275319379716, 1.000000000000000000) ) ) 
 REPRESENTATION_ITEM ( '' )  SURFACE ( )  );
#16613=CARTESIAN_POINT ( 'NONE',  ( 0.1756478951291680912, -4.720212513052437941, -3.169390900447856652 ) ) ;
#16615=ORIENTED_EDGE ( 'NONE', *, *, #13004, .F. ) ;
#16625=ORIENTED_EDGE ( 'NONE', *, *, #16868, .T. ) ;
#16633=ORIENTED_EDGE ( 'NONE', *, *, #2225, .T. ) ;
#16646=CARTESIAN_POINT ( 'NONE',  ( -4.000000000000000000, -1.942223658245630480, -0.3516579909967653128 ) ) ;
#16653=DIRECTION ( 'NONE',  ( 0.000000000000000000, 0.000000000000000000, 1.000000000000000000 ) ) ;
#16661=ORIENTED_EDGE ( 'NONE', *, *, #5761, .T. ) ;
#16685=CARTESIAN_POINT ( 'NONE',  ( 3.199999999999999289, 0.000000000000000000, 2.399999999999999467 ) ) ;
#16703=VERTEX_POINT ( 'NONE', #17712 ) ;
#16716=DIRECTION ( 'NONE',  ( -1.000000000000000000, 0.000000000000000000, 0.000000000000000000 ) ) ;
#16729=VERTEX_POINT ( 'NONE', #1886 ) ;
#16735=CARTESIAN_POINT ( 'NONE',  ( -4.000000000000000888, 1.563622288139197458, -0.2253451193528329122 ) ) ;
#16760=LINE ( 'NONE', #4510, #16791 ) ;
#16783=CONICAL_SURFACE ( 'NONE', #11239, 2.540000000000001368, 0.7853981633974502774 ) ;
#16791=VECTOR ( 'NONE', #11473, 1000.000000000000000 ) ;
#16808=ORIENTED_EDGE ( 'NONE', *, *, #9739, .F. ) ;
#16814=CARTESIAN_POINT ( 'NONE',  ( 4.197310878070204865, 0.8178547585014688259, -3.202500312981938269 ) ) ;
#16827=ORIENTED_EDGE ( 'NONE', *, *, #2848, .T. ) ;
#16835=CARTESIAN_POINT ( 'NONE',  ( 0.000000000000000000, 0.000000000000000000, 1.159999999999999476 ) ) ;
#16852=DIRECTION ( 'NONE',  ( 1.000000000000000000, 0.000000000000000000, 0.000000000000000000 ) ) ;
#16861=DIRECTION ( 'NONE',  ( 1.224646799147353207E-16, 1.000000000000000000, 0.000000000000000000 ) ) ;
#16863=VERTEX_POINT ( 'NONE', #1382 ) ;
#16868=EDGE_CURVE ( 'NONE', #9939, #7023, #5606, .T. ) ;
#16904=VECTOR ( 'NONE', #17661, 1000.000000000000000 ) ;
#16915=LINE ( 'NONE', #12812, #4546 ) ;
#16937=ORIENTED_EDGE ( 'NONE', *, *, #3228, .T. ) ;
#16943=VERTEX_POINT ( 'NONE', #6904 ) ;
#16945=DIRECTION ( 'NONE',  ( -0.000000000000000000, -0.000000000000000000, 1.000000000000000000 ) ) ;
#16960=ORIENTED_EDGE ( 'NONE', *, *, #8484, .F. ) ;
#16969=CARTESIAN_POINT ( 'NONE',  ( -3.999999999999998224, 0.000000000000000000, 0.000000000000000000 ) ) ;
#16975=CARTESIAN_POINT ( 'NONE',  ( 0.000000000000000000, 0.000000000000000000, 0.000000000000000000 ) ) ;
#17025=AXIS2_PLACEMENT_3D ( 'NONE', #5022, #5281, #16373 ) ;
#17096=ORIENTED_EDGE ( 'NONE', *, *, #2534, .T. ) ;
#17101=EDGE_LOOP ( 'NONE', ( #9149, #16937, #6909, #11192, #7639 ) ) ;
#17128=CIRCLE ( 'NONE', #10990, 3.999999999999998224 ) ;
#17130=CARTESIAN_POINT ( 'NONE',  ( -4.197477404309750249, 0.8522071663317478674, -3.205040426610024085 ) ) ;
#17137=CARTESIAN_POINT ( 'NONE',  ( 4.211140560182196957, -2.431303136016550237, -3.445885042887436800 ) ) ;
#17199=ORIENTED_EDGE ( 'NONE', *, *, #10886, .F. ) ;
#17207=CIRCLE ( 'NONE', #17516, 3.999999999999999112 ) ;
#17229=CARTESIAN_POINT ( 'NONE',  ( 2.449848172108562316, 3.432307619358737849, -3.203702292528906259 ) ) ;
#17235=FILL_AREA_STYLE ('',( #11667 ) ) ;
#17241=EDGE_LOOP ( 'NONE', ( #1634, #2586, #3745, #6196 ) ) ;
#17270=B_SPLINE_CURVE_WITH_KNOTS ( 'NONE', 3,
 ( #9863, #15418, #3271, #5883, #7087, #1644 ),
 .UNSPECIFIED., .F., .F.,
 ( 4, 2, 4 ),
 ( 0.002365888236227972966, 0.003551327329835079344, 0.004736766423442184855 ),
 .UNSPECIFIED. ) ;
#17284=ORIENTED_EDGE ( 'NONE', *, *, #1084, .F. ) ;
#17285=DIRECTION ( 'NONE',  ( 1.000000000000000000, 0.000000000000000000, 0.000000000000000000 ) ) ;
#17312=CARTESIAN_POINT ( 'NONE',  ( -3.349226789952655547, -2.685125164760741256, -0.2236248678334855911 ) ) ;
#17314=CARTESIAN_POINT ( 'NONE',  ( 0.000000000000000000, 0.000000000000000000, 2.399999999999999467 ) ) ;
#17352=CARTESIAN_POINT ( 'NONE',  ( 3.355112389629170355, -2.681727112203166730, -0.2256878752776763641 ) ) ;
#17364=ORIENTED_EDGE ( 'NONE', *, *, #10152, .F. ) ;
#17369=CARTESIAN_POINT ( 'NONE',  ( 4.141042022537587464, -2.227970427079385640, -3.387027626239166089 ) ) ;
#17383=CARTESIAN_POINT ( 'NONE',  ( -1.144235203016674918, -3.958177651039095135, -0.09382832055446259367 ) ) ;
#17395=CARTESIAN_POINT ( 'NONE',  ( -0.6920835326022560796, -4.454600218803894229, -3.297382984111586257 ) ) ;
#17404=EDGE_LOOP ( 'NONE', ( #7343, #11870, #3015 ) ) ;
#17406=EDGE_CURVE ( 'NONE', #2327, #3955, #11563, .T. ) ;
#17409=CARTESIAN_POINT ( 'NONE',  ( -4.101948962585906244, -2.368261337751083939, -3.381124513963624345 ) ) ;
#17440=CARTESIAN_POINT ( 'NONE',  ( -7.511572993685817836E-16, -4.618802153517020059, -3.133295621305386636 ) ) ;
#17471=CARTESIAN_POINT ( 'NONE',  ( 0.5449245075115098924, 4.304189842417216028, -3.016622336523194114 ) ) ;
#17516=AXIS2_PLACEMENT_3D ( 'NONE', #15969, #7707, #11773 ) ;
#17524=EDGE_CURVE ( 'NONE', #8513, #3428, #5291, .T. ) ;
#17540=B_SPLINE_CURVE_WITH_KNOTS ( 'NONE', 3,
 ( #4987, #3644, #13159, #10515, #10327, #5073, #15882, #6077 ),
 .UNSPECIFIED., .F., .F.,
 ( 4, 2, 2, 4 ),
 ( 0.005725059856848630467, 0.006314084072593618806, 0.006903108288338607144, 0.008081156719828584689 ),
 .UNSPECIFIED. ) ;
#17575=DIRECTION ( 'NONE',  ( 0.000000000000000000, 0.000000000000000000, 1.000000000000000000 ) ) ;
#17603=CARTESIAN_POINT ( 'NONE',  ( 4.197393957002304887, 7.725818140447171444E-14, -3.203767560748932208 ) ) ;
#17607=DIRECTION ( 'NONE',  ( -0.5000000000000014433, -0.8660254037844378194, 0.000000000000000000 ) ) ;
#17644=CARTESIAN_POINT ( 'NONE',  ( 2.725758460532925920, -3.045084772582431043, -2.920601398289156769 ) ) ;
#17647=CONICAL_SURFACE ( 'NONE', #2541, 2.540000000000001368, 0.7853981633974502774 ) ;
#17648=CARTESIAN_POINT ( 'NONE',  ( 8.409399735147211686E-16, 4.618802153517009401, -3.133295621305383083 ) ) ;
#17661=DIRECTION ( 'NONE',  ( -0.000000000000000000, -0.000000000000000000, 1.000000000000000000 ) ) ;
#17664=CARTESIAN_POINT ( 'NONE',  ( 3.999999999999999112, 2.309401076758498927, -3.204271511726786148 ) ) ;
#17712=CARTESIAN_POINT ( 'NONE',  ( -2.000000000000002220, 3.464101615137751278, 0.000000000000000000 ) ) ;
#17724=CLOSED_SHELL ( 'NONE', ( #935, #2564, #16166, #5969, #4132, #4045, #13818, #1930, #12101, #7035, #2427, #6780, #6875, #12445, #14907, #15471, #14160, #15459, #9541, #4313, #795, #11321, #16064, #13285, #10399, #13111, #1748, #7311, #4063, #5729, #2670, #734, #14942, #4690, #8578, #889, #6946, #8723, #12873 ) ) ;
#17754=CARTESIAN_POINT ( 'NONE',  ( 4.101954839143060916, -2.368264730582942956, -3.381130640444271584 ) ) ;
#17769=AXIS2_PLACEMENT_3D ( 'NONE', #552, #17607, #5045 ) ;
#17797=CARTESIAN_POINT ( 'NONE',  ( -4.000000000000000000, -2.309401076758510918, -0.5000000000000000000 ) ) ;
#17801=DIRECTION ( 'NONE',  ( -0.5000000000000008882, 0.8660254037844382635, 0.000000000000000000 ) ) ;
#17817=DIRECTION ( 'NONE',  ( 0.000000000000000000, 0.000000000000000000, 1.000000000000000000 ) ) ;
#17824=DIRECTION ( 'NONE',  ( -0.000000000000000000, -0.000000000000000000, 1.000000000000000000 ) ) ;
#17837=DIRECTION ( 'NONE',  ( -0.000000000000000000, -0.000000000000000000, 1.000000000000000000 ) ) ;
#17844=PLANE ( 'NONE',  #10392 ) ;
#17845=CARTESIAN_POINT ( 'NONE',  ( 4.000000000000000000, -2.511476383524240408, -3.169254053377044134 ) ) ;
#17848=DIRECTION ( 'NONE',  ( -0.000000000000000000, -0.000000000000000000, 1.000000000000000000 ) ) ;
#17859=DIRECTION ( 'NONE',  ( -0.000000000000000000, -0.000000000000000000, 1.000000000000000000 ) ) ;
#17863=SURFACE_STYLE_USAGE ( .BOTH. , #10995 ) ;
#17891=ORIENTED_EDGE ( 'NONE', *, *, #3228, .F. ) ;
#17903=CARTESIAN_POINT ( 'NONE',  ( 3.333333333333333481, 2.694301256218250007, -3.000726591567081325 ) ) ;
#17916=CONICAL_SURFACE ( 'NONE', #5999, 3.999999999999998224, 0.8911886515913775009 ) ;
#17927=EDGE_LOOP ( 'NONE', ( #11998, #11398, #16142, #732 ) ) ;
#17928=STYLED_ITEM ( 'NONE', ( #13225 ), #5349 ) ;
#17944=CYLINDRICAL_SURFACE ( 'NONE', #15130, 2.500000000000000888 ) ;
ENDSEC;
END-ISO-10303-21;
